ISO-10303-21;
HEADER;
FILE_DESCRIPTION (('STEP AP214'),
    '1' );
FILE_NAME ('torque nut 08a_iso_ISO 10511-M8-N.step',
    '2026-10-08T13:46:47',
    ( '' ),
    ( '' ),
    'SwSTEP 2.0',
    'SolidWorks 2026',
    '' );
FILE_SCHEMA (( 'AUTOMOTIVE_DESIGN' ));
ENDSEC;

DATA;
#6=DIRECTION ( 'NONE',  ( -0.000000000000000000, -0.000000000000000000, 1.000000000000000000 ) ) ;
#13=CARTESIAN_POINT ( 'NONE',  ( -1.656854249492380804, 4.000000000000000000, 6.112500000000002487 ) ) ;
#30=CARTESIAN_POINT ( 'NONE',  ( -2.449293598294706907E-16, 4.000000000000000000, 7.613708498984758322 ) ) ;
#42=EDGE_LOOP ( 'NONE', ( #8288, #11668, #9814 ) ) ;
#47=CARTESIAN_POINT ( 'NONE',  ( -1.656854249492380804, 4.000000000000000000, -3.762499997268812013 ) ) ;
#49=DIRECTION ( 'NONE',  ( 1.000000000000000000, 0.000000000000000000, 0.000000000000000000 ) ) ;
#52=CARTESIAN_POINT ( 'NONE',  ( 4.000000000000000000, 4.898587196589412829E-16, -2.199999999999998845 ) ) ;
#58=CARTESIAN_POINT ( 'NONE',  ( 1.432654583217642053, -3.458734124999999882, 0.3000000013655960140 ) ) ;
#61=CARTESIAN_POINT ( 'NONE',  ( -4.000000000000000000, 4.898587196589412829E-16, 19.04999999999996874 ) ) ;
#63=CARTESIAN_POINT ( 'NONE',  ( 1.432654583217642275, -3.458734124999999437, -1.949999998634404319 ) ) ;
#66=CARTESIAN_POINT ( 'NONE',  ( 4.000000000000000000, 4.898587196589412829E-16, -0.1999999999999987899 ) ) ;
#85=CARTESIAN_POINT ( 'NONE',  ( 2.828427124746190735, -2.828427124746189847, -0.3249999999999971800 ) ) ;
#111=DIRECTION ( 'NONE',  ( 0.5000000000000006661, 0.8660254037844382635, -0.000000000000000000 ) ) ;
#113=CARTESIAN_POINT ( 'NONE',  ( -3.462118672051860191, 1.261024841198670421, -3.429387741257551081 ) ) ;
#123=CARTESIAN_POINT ( 'NONE',  ( -4.000000000000000000, 0.000000000000000000, 5.300000000000000711 ) ) ;
#137=EDGE_CURVE ( 'NONE', #15758, #669, #1279, .T. ) ;
#142=ADVANCED_FACE ( 'NONE', ( #17693 ), #8211, .T. ) ;
#143=AXIS2_PLACEMENT_3D ( 'NONE', #14347, #4748, #19821 ) ;
#147=EDGE_CURVE ( 'NONE', #12600, #6989, #10767, .T. ) ;
#155=ORIENTED_EDGE ( 'NONE', *, *, #6433, .T. ) ;
#161=CARTESIAN_POINT ( 'NONE',  ( -4.000000000000000000, 0.000000000000000000, -3.574999997268813345 ) ) ;
#175=AXIS2_PLACEMENT_3D ( 'NONE', #8755, #4676, #12125 ) ;
#179=CARTESIAN_POINT ( 'NONE',  ( -2.445694354108819635, -2.445694354108820523, -1.137499998634402765 ) ) ;
#193=ORIENTED_EDGE ( 'NONE', *, *, #20761, .T. ) ;
#203=CARTESIAN_POINT ( 'NONE',  ( -2.449293598294706907E-16, 4.000000000000000000, 0.1750000027311865991 ) ) ;
#227=FACE_OUTER_BOUND ( 'NONE', #6243, .T. ) ;
#232=DIRECTION ( 'NONE',  ( -0.000000000000000000, -0.000000000000000000, 1.000000000000000000 ) ) ;
#236=CARTESIAN_POINT ( 'NONE',  ( 1.432654583217642275, -3.458734124999999882, -2.699999998634404541 ) ) ;
#237=CARTESIAN_POINT ( 'NONE',  ( -2.828427124746190291, 2.828427124746190291, 6.175000000000001599 ) ) ;
#240=ORIENTED_EDGE ( 'NONE', *, *, #11094, .F. ) ;
#247=EDGE_CURVE ( 'NONE', #438, #3610, #9877, .T. ) ;
#271=CYLINDRICAL_SURFACE ( 'NONE', #5922, 4.714285714285714413 ) ;
#274=CARTESIAN_POINT ( 'NONE',  ( 3.458734125000000770, -1.432654583217639610, 4.175000001365593683 ) ) ;
#293=CARTESIAN_POINT ( 'NONE',  ( 3.458734125000000326, 1.432654583217640498, 0.3000000013655960696 ) ) ;
#314=CARTESIAN_POINT ( 'NONE',  ( -6.500000000000000000, -3.752776749732573247, -0.5805565836007695601 ) ) ;
#322=ORIENTED_EDGE ( 'NONE', *, *, #7035, .T. ) ;
#324=CARTESIAN_POINT ( 'NONE',  ( -2.828427124746190291, 2.828427124746190291, 0.3000000027311867101 ) ) ;
#330=CARTESIAN_POINT ( 'NONE',  ( 1.656854249492383024, -3.999999999999999112, 0.6125000000000022649 ) ) ;
#331=CARTESIAN_POINT ( 'NONE',  ( -1.301042606982605321E-15, 7.505553499465137612, -0.5805565836007695601 ) ) ;
#342=EDGE_CURVE ( 'NONE', #20113, #6042, #11222, .T. ) ;
#352=CARTESIAN_POINT ( 'NONE',  ( 2.149474931388133836, 6.264553569211843254, -3.644669744206378681 ) ) ;
#359=CARTESIAN_POINT ( 'NONE',  ( 0.000000000000000000, 0.000000000000000000, 0.000000000000000000 ) ) ;
#363=CARTESIAN_POINT ( 'NONE',  ( -2.445694354108820523, 2.445694354108820523, -2.137499998634403653 ) ) ;
#365=CARTESIAN_POINT ( 'NONE',  ( 4.000000000000000000, 1.656854249492381248, 1.862500000000001599 ) ) ;
#376=CARTESIAN_POINT ( 'NONE',  ( -2.828427124746190291, 2.828427124746190291, 1.300000002731187543 ) ) ;
#406=CARTESIAN_POINT ( 'NONE',  ( 4.000000000000000000, 1.656854249492381248, -2.012499997268811569 ) ) ;
#414=CARTESIAN_POINT ( 'NONE',  ( -3.458734125000000326, -1.432654583217642497, 1.050000001365596791 ) ) ;
#422=CARTESIAN_POINT ( 'NONE',  ( -2.445694354108819635, -2.445694354108820523, -2.137499998634403653 ) ) ;
#438=VERTEX_POINT ( 'NONE', #2331 ) ;
#451=CARTESIAN_POINT ( 'NONE',  ( -1.647987302177966740E-14, -7.505553499465137612, -3.119443416399232394 ) ) ;
#461=B_SPLINE_CURVE_WITH_KNOTS ( 'NONE', 3,
 ( #13230, #10227, #23012, #13936, #854, #2656 ),
 .UNSPECIFIED., .F., .F.,
 ( 4, 2, 4 ),
 ( 0.006695446894088488872, 0.008593684019695166376, 0.01049192114530184475 ),
 .UNSPECIFIED. ) ;
#485=CARTESIAN_POINT ( 'NONE',  ( -2.445694354108819635, -2.445694354108820967, -0.8874999986344025427 ) ) ;
#486=CARTESIAN_POINT ( 'NONE',  ( 4.000000000000000000, 4.898587196589412829E-16, 0.8000000000000020428 ) ) ;
#490=ORIENTED_EDGE ( 'NONE', *, *, #671, .F. ) ;
#509=CARTESIAN_POINT ( 'NONE',  ( -2.445694354108820523, 2.445694354108820523, 2.862500001365597235 ) ) ;
#518=PRESENTATION_STYLE_ASSIGNMENT (( #3876 ) ) ;
#519=CARTESIAN_POINT ( 'NONE',  ( 3.458734125000000326, 4.235727675282971730E-16, 2.237500001365596791 ) ) ;
#530=CARTESIAN_POINT ( 'NONE',  ( -3.525817189091416282, -5.469921996229804684, -3.700000000000000622 ) ) ;
#535=CARTESIAN_POINT ( 'NONE',  ( -1.432654583217641164, -3.458734125000000326, 4.175000001365593683 ) ) ;
#542=CARTESIAN_POINT ( 'NONE',  ( 1.656854249492380360, 4.000000000000000000, 5.112500002731189319 ) ) ;
#556=CIRCLE ( 'NONE', #10551, 4.000000000000000000 ) ;
#580=( BOUNDED_CURVE ( )  B_SPLINE_CURVE ( 2, ( #16295, #1659, #8523, #12481, #6712, #3467, #17625, #14148, #21414 ),
 .UNSPECIFIED., .F., .F. ) 
 B_SPLINE_CURVE_WITH_KNOTS ( ( 3, 2, 2, 2, 3 ),
 ( 0.4500000000000000111, 0.4625000000000000222, 0.4749999999999999778, 0.4874999999999999889, 0.5000000000000000000 ),
 .UNSPECIFIED. ) 
 CURVE ( )  GEOMETRIC_REPRESENTATION_ITEM ( )  RATIONAL_B_SPLINE_CURVE ( ( 1.000000000000000000, 0.9238795325112867385, 1.000000000000000000, 0.9238795325112867385, 1.000000000000000000, 0.9238795325112867385, 1.000000000000000000, 0.9238795325112867385, 1.000000000000000000 ) ) 
 REPRESENTATION_ITEM ( '' )  );
#597=CARTESIAN_POINT ( 'NONE',  ( 1.656854249492380360, 4.000000000000000000, 1.987500000000001599 ) ) ;
#612=ADVANCED_FACE ( 'NONE', ( #9398 ), #13898, .F. ) ;
#624=CARTESIAN_POINT ( 'NONE',  ( -2.117863837641485618E-16, 3.458734125000000770, 4.737500001365595459 ) ) ;
#628=FACE_OUTER_BOUND ( 'NONE', #9210, .T. ) ;
#631=CARTESIAN_POINT ( 'NONE',  ( 6.353591512924457348E-16, -3.458734125000000326, 1.987500001365596569 ) ) ;
#637=DIRECTION ( 'NONE',  ( -0.000000000000000000, -0.000000000000000000, 1.000000000000000000 ) ) ;
#642=CARTESIAN_POINT ( 'NONE',  ( 2.445694354108820079, 2.445694354108820523, -1.387499998634402987 ) ) ;
#650=CARTESIAN_POINT ( 'NONE',  ( -2.117863837641485618E-16, 3.458734125000000770, 5.737500001365596347 ) ) ;
#657=CARTESIAN_POINT ( 'NONE',  ( 4.000000000000000000, 4.898587196589412829E-16, 4.925000002731187543 ) ) ;
#661=CARTESIAN_POINT ( 'NONE',  ( 2.828427124746190735, -2.828427124746189847, 1.800000002731187987 ) ) ;
#663=EDGE_LOOP ( 'NONE', ( #15328, #14805, #193, #15082 ) ) ;
#666=UNCERTAINTY_MEASURE_WITH_UNIT (LENGTH_MEASURE( 1.000000000000000082E-05 ), #20509, 'distance_accuracy_value', 'NONE');
#669=VERTEX_POINT ( 'NONE', #23212 ) ;
#671=EDGE_CURVE ( 'NONE', #1632, #19016, #6131, .T. ) ;
#685=CARTESIAN_POINT ( 'NONE',  ( 3.007318562400188799, 2.637429632093199139, 2.039999999999998259 ) ) ;
#708=ADVANCED_FACE ( 'NONE', ( #10683 ), #16403, .F. ) ;
#715=CARTESIAN_POINT ( 'NONE',  ( 6.500000000000002665, 1.277696550142691345, -0.05601745114479450560 ) ) ;
#717=CARTESIAN_POINT ( 'NONE',  ( -2.449293598294706907E-16, 4.000000000000000000, 1.050000000000000488 ) ) ;
#720=CARTESIAN_POINT ( 'NONE',  ( 1.656854249492380138, 4.000000000000000000, -1.012499999999997291 ) ) ;
#747=CARTESIAN_POINT ( 'NONE',  ( 1.432654583217642275, -3.458734124999999882, 3.300000001365598568 ) ) ;
#752=ADVANCED_FACE ( 'NONE', ( #2001 ), #7785, .T. ) ;
#757=ORIENTED_EDGE ( 'NONE', *, *, #9423, .F. ) ;
#760=CARTESIAN_POINT ( 'NONE',  ( 1.432654583217639832, 3.458734125000000326, 1.425000001365596791 ) ) ;
#761=CARTESIAN_POINT ( 'NONE',  ( 2.445694354108820523, -2.445694354108820079, -0.8874999986344025427 ) ) ;
#769=CARTESIAN_POINT ( 'NONE',  ( 1.432654583217642053, -3.458734124999999882, -1.699999998634403875 ) ) ;
#779=CARTESIAN_POINT ( 'NONE',  ( -1.432654583217640942, -3.458734124999999882, -3.074999998634404541 ) ) ;
#782=LINE ( 'NONE', #8468, #11502 ) ;
#787=ORIENTED_EDGE ( 'NONE', *, *, #23119, .F. ) ;
#789=CARTESIAN_POINT ( 'NONE',  ( -2.828427124746190291, 2.828427124746190291, 5.300000002731187543 ) ) ;
#794=DIRECTION ( 'NONE',  ( 1.000000000000000000, 0.000000000000000000, 0.000000000000000000 ) ) ;
#834=CARTESIAN_POINT ( 'NONE',  ( -1.656854249492381248, -3.999999999999999112, 0.4875000000000020983 ) ) ;
#837=ORIENTED_EDGE ( 'NONE', *, *, #7035, .F. ) ;
#844=VERTEX_POINT ( 'NONE', #16632 ) ;
#854=CARTESIAN_POINT ( 'NONE',  ( 6.500000000000000000, -0.6341575537611441327, 4.794206481459339919E-16 ) ) ;
#857=CARTESIAN_POINT ( 'NONE',  ( 3.458734125000000770, 1.432654583217640498, 3.550000001365598568 ) ) ;
#865=CARTESIAN_POINT ( 'NONE',  ( 3.458734125000000770, -1.432654583217639610, 0.1750000013655959585 ) ) ;
#866=CARTESIAN_POINT ( 'NONE',  ( -3.458734125000000326, 1.432654583217640276, -0.3249999986344045411 ) ) ;
#886=CARTESIAN_POINT ( 'NONE',  ( -1.432654583217641164, -3.458734125000000326, 5.175000001365595459 ) ) ;
#895=CARTESIAN_POINT ( 'NONE',  ( 2.828427124746189847, 2.828427124746190291, 5.050000002731187543 ) ) ;
#898=CARTESIAN_POINT ( 'NONE',  ( 1.656854249492383024, -3.999999999999999112, 1.737500002731187543 ) ) ;
#933=CARTESIAN_POINT ( 'NONE',  ( -4.350525068611871049, 4.993776679985853839, -0.05533025579362114976 ) ) ;
#936=ORIENTED_EDGE ( 'NONE', *, *, #12706, .F. ) ;
#959=( BOUNDED_CURVE ( )  B_SPLINE_CURVE ( 2, ( #685, #9940, #4405 ),
 .UNSPECIFIED., .F., .F. ) 
 B_SPLINE_CURVE_WITH_KNOTS ( ( 3, 3 ),
 ( 0.3385621442156623861, 0.3499999999999999778 ),
 .UNSPECIFIED. ) 
 CURVE ( )  GEOMETRIC_REPRESENTATION_ITEM ( )  RATIONAL_B_SPLINE_CURVE ( ( 0.9881630579574953721, 0.9303476056502189007, 1.000000000000000000 ) ) 
 REPRESENTATION_ITEM ( '' )  );
#973=CARTESIAN_POINT ( 'NONE',  ( 3.458734125000001214, -1.432654583217639610, 3.425000001365596791 ) ) ;
#981=ORIENTED_EDGE ( 'NONE', *, *, #2562, .T. ) ;
#984=CARTESIAN_POINT ( 'NONE',  ( -2.445694354108820523, 2.445694354108820523, 0.6125000013655953479 ) ) ;
#986=CARTESIAN_POINT ( 'NONE',  ( 3.458734125000000326, 1.432654583217640498, 1.300000001365597013 ) ) ;
#989=SURFACE_STYLE_FILL_AREA ( #6166 ) ;
#1005=CARTESIAN_POINT ( 'NONE',  ( -1.432654583217641164, -3.458734125000000326, 3.175000001365598568 ) ) ;
#1010=PLANE ( 'NONE',  #8594 ) ;
#1030=CARTESIAN_POINT ( 'NONE',  ( 1.432654583217642275, -3.458734124999999437, 4.050000001365596347 ) ) ;
#1055=EDGE_LOOP ( 'NONE', ( #23220, #8381, #22152 ) ) ;
#1064=CARTESIAN_POINT ( 'NONE',  ( 2.828427124746189847, 2.828427124746190291, -1.074999999999997735 ) ) ;
#1071=CARTESIAN_POINT ( 'NONE',  ( 6.499999999999999112, -3.752776749732574135, -0.5805565836007695601 ) ) ;
#1077=ORIENTED_EDGE ( 'NONE', *, *, #7147, .T. ) ;
#1079=ORIENTED_EDGE ( 'NONE', *, *, #15144, .F. ) ;
#1089=CARTESIAN_POINT ( 'NONE',  ( 2.445694354108820079, 2.445694354108820523, -1.387499998634402987 ) ) ;
#1093=CARTESIAN_POINT ( 'NONE',  ( 0.000000000000000000, 0.000000000000000000, 2.039999999999998259 ) ) ;
#1100=CARTESIAN_POINT ( 'NONE',  ( -2.445694354108819635, -2.445694354108820523, 0.8625000013655955700 ) ) ;
#1102=CARTESIAN_POINT ( 'NONE',  ( -4.000000000000000000, 0.000000000000000000, 1.300000000000000711 ) ) ;
#1121=CARTESIAN_POINT ( 'NONE',  ( 6.353591512924457348E-16, -3.458734125000000770, 2.237500001365596791 ) ) ;
#1130=CARTESIAN_POINT ( 'NONE',  ( -2.828427124746189403, -2.828427124746190735, -0.4499999972688122352 ) ) ;
#1149=CARTESIAN_POINT ( 'NONE',  ( 2.445694354108820079, 2.445694354108820523, 5.362500001365596347 ) ) ;
#1168=EDGE_CURVE ( 'NONE', #10566, #15405, #10231, .T. ) ;
#1185=CARTESIAN_POINT ( 'NONE',  ( 7.347880794884118750E-16, -4.000000000000000000, -1.449999999999998179 ) ) ;
#1206=CARTESIAN_POINT ( 'NONE',  ( 3.458734125000001214, -1.432654583217639610, -0.5749999986344027647 ) ) ;
#1217=EDGE_LOOP ( 'NONE', ( #8451, #11418 ) ) ;
#1226=LINE ( 'NONE', #8564, #6844 ) ;
#1232=CARTESIAN_POINT ( 'NONE',  ( 3.458734125000001214, -1.432654583217639610, 2.425000001365597679 ) ) ;
#1243=CARTESIAN_POINT ( 'NONE',  ( -4.000000000000000000, 0.000000000000000000, 0.4250000027311868211 ) ) ;
#1246=CARTESIAN_POINT ( 'NONE',  ( 1.876855952934447513, -6.421950209808290566, -0.1061556211655389631 ) ) ;
#1258=CARTESIAN_POINT ( 'NONE',  ( -3.458734124999999882, -1.432654583217642497, 2.800000001365598123 ) ) ;
#1265=CARTESIAN_POINT ( 'NONE',  ( -2.710465755160788248, 2.627675682436018789, 2.039999999999999591 ) ) ;
#1279=CIRCLE ( 'NONE', #14335, 6.500000000000000888 ) ;
#1308=ORIENTED_EDGE ( 'NONE', *, *, #15835, .T. ) ;
#1319=CARTESIAN_POINT ( 'NONE',  ( 2.445694354108820079, 2.445694354108820523, 1.612500001365596125 ) ) ;
#1325=VERTEX_POINT ( 'NONE', #18370 ) ;
#1326=CARTESIAN_POINT ( 'NONE',  ( 4.000000000000000000, 4.898587196589412829E-16, -3.074999997268812901 ) ) ;
#1337=ORIENTED_EDGE ( 'NONE', *, *, #14917, .F. ) ;
#1353=CARTESIAN_POINT ( 'NONE',  ( -1.432654583217640498, 3.458734125000000770, 0.8000000013655964581 ) ) ;
#1354=CARTESIAN_POINT ( 'NONE',  ( -3.100354668897359112, -1.549725627487283042, 2.039999999999999591 ) ) ;
#1356=B_SPLINE_CURVE_WITH_KNOTS ( 'NONE', 3,
 ( #20698, #2494, #3942, #7555, #20457, #16897 ),
 .UNSPECIFIED., .F., .F.,
 ( 4, 2, 4 ),
 ( 2.380733003178814001E-07, 0.001898835937927378101, 0.003797433802554438069 ),
 .UNSPECIFIED. ) ;
#1361=CARTESIAN_POINT ( 'NONE',  ( -4.000000000000000000, 0.000000000000000000, -0.5749999972688123462 ) ) ;
#1376=CARTESIAN_POINT ( 'NONE',  ( -2.445694354108820523, 2.445694354108820523, 2.612500001365597235 ) ) ;
#1396=CARTESIAN_POINT ( 'NONE',  ( -4.000000000000000000, 0.000000000000000000, -0.6999999999999975131 ) ) ;
#1401=EDGE_CURVE ( 'NONE', #18845, #18467, #22431, .T. ) ;
#1407=DIRECTION ( 'NONE',  ( 1.000000000000000000, 0.000000000000000000, 0.000000000000000000 ) ) ;
#1413=FACE_OUTER_BOUND ( 'NONE', #7586, .T. ) ;
#1414=CARTESIAN_POINT ( 'NONE',  ( 3.458734125000000326, 1.432654583217640498, -0.6999999986344048741 ) ) ;
#1420=FACE_OUTER_BOUND ( 'NONE', #1217, .T. ) ;
#1422=B_SPLINE_CURVE_WITH_KNOTS ( 'NONE', 3,
 ( #8160, #15471, #15360, #2388, #16902, #18558, #22501, #13443 ),
 .UNSPECIFIED., .F., .F.,
 ( 4, 2, 2, 4 ),
 ( 0.003797433802554446743, 0.004743183970586241360, 0.005688934138618037713, 0.007580434474681626081 ),
 .UNSPECIFIED. ) ;
#1439=CARTESIAN_POINT ( 'NONE',  ( -2.445694354108820523, 2.445694354108820523, -2.137499998634403653 ) ) ;
#1452=CARTESIAN_POINT ( 'NONE',  ( -3.458734125000000326, 1.432654583217640276, -2.324999998634404097 ) ) ;
#1460=AXIS2_PLACEMENT_3D ( 'NONE', #4182, #2261, #11163 ) ;
#1473=CARTESIAN_POINT ( 'NONE',  ( -3.458734125000000770, 0.000000000000000000, 1.987500001365596569 ) ) ;
#1474=CARTESIAN_POINT ( 'NONE',  ( -1.914603566986515348, -2.889253230644202031, 2.039999999999998703 ) ) ;
#1483=CARTESIAN_POINT ( 'NONE',  ( -4.000000000000000000, -1.656854249492383246, 1.487500002731187543 ) ) ;
#1490=LINE ( 'NONE', #8831, #18279 ) ;
#1499=CARTESIAN_POINT ( 'NONE',  ( 0.000000000000000000, 0.000000000000000000, 2.039999999999998259 ) ) ;
#1508=CARTESIAN_POINT ( 'NONE',  ( 2.445694354108820079, 2.445694354108820523, 4.362500001365595459 ) ) ;
#1510=CARTESIAN_POINT ( 'NONE',  ( -2.449293598294706907E-16, 4.000000000000000000, 0.05000000000000143219 ) ) ;
#1512=EDGE_LOOP ( 'NONE', ( #7438, #8198, #13441, #21564, #11897, #1337 ) ) ;
#1524=CIRCLE ( 'NONE', #13801, 4.000000000000000000 ) ;
#1546=CARTESIAN_POINT ( 'NONE',  ( 2.445694354108820079, 2.445694354108820523, -0.6374999986344040970 ) ) ;
#1556=FACE_OUTER_BOUND ( 'NONE', #21064, .T. ) ;
#1563=CARTESIAN_POINT ( 'NONE',  ( 2.445694354108820079, 2.445694354108820523, -0.3874999986344038194 ) ) ;
#1576=CARTESIAN_POINT ( 'NONE',  ( 1.432654583217642053, -3.458734124999999437, -2.949999998634404985 ) ) ;
#1580=DIRECTION ( 'NONE',  ( 0.000000000000000000, 0.000000000000000000, 1.000000000000000000 ) ) ;
#1589=CARTESIAN_POINT ( 'NONE',  ( -4.000000000000000000, 0.000000000000000000, -2.574999997268812457 ) ) ;
#1594=CARTESIAN_POINT ( 'NONE',  ( 1.432654583217640276, 3.458734125000000770, -2.324999998634404097 ) ) ;
#1595=CARTESIAN_POINT ( 'NONE',  ( -2.872501113216805901, -1.939738628788093999, 2.039999999999998703 ) ) ;
#1602=CARTESIAN_POINT ( 'NONE',  ( -1.656854249492381248, -3.999999999999999112, -0.3874999972688123462 ) ) ;
#1603=EDGE_CURVE ( 'NONE', #13238, #7689, #17892, .T. ) ;
#1614=EDGE_LOOP ( 'NONE', ( #12666, #11057, #5802 ) ) ;
#1622=CARTESIAN_POINT ( 'NONE',  ( -2.445694354108820523, 2.445694354108820523, 1.612500001365596125 ) ) ;
#1627=EDGE_LOOP ( 'NONE', ( #4407, #12067, #3715, #23565 ) ) ;
#1632=VERTEX_POINT ( 'NONE', #14203 ) ;
#1659=CARTESIAN_POINT ( 'NONE',  ( 4.000000000000000888, -1.656854249492379694, 0.8625000027311868767 ) ) ;
#1663=CARTESIAN_POINT ( 'NONE',  ( -3.458734125000000326, 0.000000000000000000, -2.262499998634403653 ) ) ;
#1677=DIRECTION ( 'NONE',  ( 1.000000000000000000, 0.000000000000000000, 0.000000000000000000 ) ) ;
#1680=CARTESIAN_POINT ( 'NONE',  ( -1.656854249492381248, -3.999999999999999112, 3.487500000000002487 ) ) ;
#1681=CARTESIAN_POINT ( 'NONE',  ( -4.000000000000000000, -1.656854249492383024, 0.3625000000000019873 ) ) ;
#1716=CARTESIAN_POINT ( 'NONE',  ( 2.445694354108820079, 2.445694354108820523, 5.362500001365596347 ) ) ;
#1727=( BOUNDED_CURVE ( )  B_SPLINE_CURVE ( 2, ( #11098, #21719, #18143, #5334, #22191, #5563, #3416, #5680, #12676 ),
 .UNSPECIFIED., .F., .F. ) 
 B_SPLINE_CURVE_WITH_KNOTS ( ( 3, 2, 2, 2, 3 ),
 ( 0.8000000000000000444, 0.8125000000000000000, 0.8249999999999999556, 0.8375000000000000222, 0.8499999999999999778 ),
 .UNSPECIFIED. ) 
 CURVE ( )  GEOMETRIC_REPRESENTATION_ITEM ( )  RATIONAL_B_SPLINE_CURVE ( ( 1.000000000000000000, 0.9238795325112867385, 1.000000000000000000, 0.9238795325112867385, 1.000000000000000000, 0.9238795325112867385, 1.000000000000000000, 0.9238795325112867385, 1.000000000000000000 ) ) 
 REPRESENTATION_ITEM ( '' )  );
#1728=ORIENTED_EDGE ( 'NONE', *, *, #10558, .T. ) ;
#1733=ADVANCED_FACE ( 'NONE', ( #19672 ), #4509, .T. ) ;
#1735=CARTESIAN_POINT ( 'NONE',  ( -1.301042606982605321E-15, 7.505553499465137612, -3.119443416399232394 ) ) ;
#1738=CARTESIAN_POINT ( 'NONE',  ( -1.432654583217640276, 3.458734125000000326, -1.449999998634403653 ) ) ;
#1743=EDGE_CURVE ( 'NONE', #10566, #4081, #12876, .T. ) ;
#1744=AXIS2_PLACEMENT_3D ( 'NONE', #13997, #21258, #23435 ) ;
#1755=CARTESIAN_POINT ( 'NONE',  ( -6.500000000000001776, -3.142418015001832821, -0.4043611937012249746 ) ) ;
#1793=CARTESIAN_POINT ( 'NONE',  ( 4.000000000000000888, -1.656854249492379694, -0.1374999972688121241 ) ) ;
#1797=CARTESIAN_POINT ( 'NONE',  ( 7.347880794884118750E-16, -4.000000000000000000, 4.549999999999999822 ) ) ;
#1800=LINE ( 'NONE', #19650, #21017 ) ;
#1833=CARTESIAN_POINT ( 'NONE',  ( -1.432654583217640276, 3.458734125000000326, 4.550000001365596347 ) ) ;
#1845=CARTESIAN_POINT ( 'NONE',  ( 2.445694354108820967, -2.445694354108820079, 0.3625000013655968467 ) ) ;
#1852=CARTESIAN_POINT ( 'NONE',  ( 3.458734125000000770, -1.432654583217639610, -1.824999998634404097 ) ) ;
#1868=ORIENTED_EDGE ( 'NONE', *, *, #342, .F. ) ;
#1869=CARTESIAN_POINT ( 'NONE',  ( -6.500000000000000000, 0.000000000000000000, 1.734723475976807094E-15 ) ) ;
#1898=CARTESIAN_POINT ( 'NONE',  ( -3.458734125000000326, 1.432654583217640276, -3.324999998634403209 ) ) ;
#1907=EDGE_CURVE ( 'NONE', #7079, #2314, #16812, .T. ) ;
#1916=CARTESIAN_POINT ( 'NONE',  ( 4.714285714285714413, 0.000000000000000000, 9.480888224575631185 ) ) ;
#1920=CARTESIAN_POINT ( 'NONE',  ( -2.449293598294706907E-16, 4.000000000000000000, 6.050000000000001599 ) ) ;
#1939=SHAPE_REPRESENTATION ( 'torque nut 08a_iso_ISO 10511-M8-N', ( #7318 ), #9900 ) ;
#1954=CARTESIAN_POINT ( 'NONE',  ( 2.445694354108820079, 2.445694354108820523, 4.362500001365595459 ) ) ;
#1955=CARTESIAN_POINT ( 'NONE',  ( 4.000000000000000000, 4.898587196589412829E-16, 1.800000000000001155 ) ) ;
#1957=B_SPLINE_CURVE_WITH_KNOTS ( 'NONE', 3,
 ( #11259, #5735, #13064, #5846, #7780, #11378, #20319, #331 ),
 .UNSPECIFIED., .F., .F.,
 ( 4, 2, 2, 4 ),
 ( 0.003797433802554438069, 0.004743183970586236156, 0.005688934138618034243, 0.007580434474681629550 ),
 .UNSPECIFIED. ) ;
#1963=CARTESIAN_POINT ( 'NONE',  ( 6.353591512924457348E-16, -3.458734125000000770, 0.2375000013655967357 ) ) ;
#1969=CARTESIAN_POINT ( 'NONE',  ( 2.445694354108820523, -2.445694354108820079, -0.8874999986344025427 ) ) ;
#1972=DIRECTION ( 'NONE',  ( 1.000000000000000000, 0.000000000000000000, 0.000000000000000000 ) ) ;
#2001=FACE_OUTER_BOUND ( 'NONE', #18168, .T. ) ;
#2026=DIRECTION ( 'NONE',  ( 1.000000000000000000, 0.000000000000000000, 0.000000000000000000 ) ) ;
#2030=CARTESIAN_POINT ( 'NONE',  ( -2.445694354108819635, -2.445694354108820967, -2.887499998634404097 ) ) ;
#2031=CARTESIAN_POINT ( 'NONE',  ( -2.449293598294706907E-16, 4.000000000000000000, 5.050000000000000711 ) ) ;
#2032=CARTESIAN_POINT ( 'NONE',  ( 7.347880794884118750E-16, -4.000000000000000000, -3.324999997268812901 ) ) ;
#2067=CARTESIAN_POINT ( 'NONE',  ( -4.000000000000000888, 1.656854249492380804, -3.637499997268812013 ) ) ;
#2078=CARTESIAN_POINT ( 'NONE',  ( 3.458734125000001214, -1.432654583217639610, 1.425000001365597013 ) ) ;
#2080=DIRECTION ( 'NONE',  ( -0.000000000000000000, -0.000000000000000000, 1.000000000000000000 ) ) ;
#2086=CARTESIAN_POINT ( 'NONE',  ( 2.445694354108820523, -2.445694354108820079, 0.1125000013655966247 ) ) ;
#2093=CARTESIAN_POINT ( 'NONE',  ( 0.2615509004163102946, 3.991439731035835603, 2.039999999999998259 ) ) ;
#2098=DIRECTION ( 'NONE',  ( -0.000000000000000000, -0.000000000000000000, 1.000000000000000000 ) ) ;
#2109=ORIENTED_EDGE ( 'NONE', *, *, #2492, .F. ) ;
#2121=ORIENTED_EDGE ( 'NONE', *, *, #2441, .F. ) ;
#2127=CARTESIAN_POINT ( 'NONE',  ( 3.803704290982252711, -5.309483803148803638, 1.219727444046192242E-16 ) ) ;
#2148=CARTESIAN_POINT ( 'NONE',  ( -1.432654583217640498, 3.458734125000000770, -1.199999998634403431 ) ) ;
#2149=CARTESIAN_POINT ( 'NONE',  ( -4.000000000000000888, 1.656854249492380804, 4.237499999999999822 ) ) ;
#2150=CARTESIAN_POINT ( 'NONE',  ( 4.000000000000000888, -1.656854249492379694, -3.137499997268812901 ) ) ;
#2191=CARTESIAN_POINT ( 'NONE',  ( 4.000000000000000000, 4.898587196589412829E-16, -3.074999997268812901 ) ) ;
#2202=CARTESIAN_POINT ( 'NONE',  ( -3.458734125000000770, 0.000000000000000000, 1.987500001365596569 ) ) ;
#2204=ADVANCED_FACE ( 'NONE', ( #10963 ), #18860, .T. ) ;
#2209=CARTESIAN_POINT ( 'NONE',  ( -2.117863837641485618E-16, 3.458734125000000770, 4.737500001365595459 ) ) ;
#2217=DIRECTION ( 'NONE',  ( -0.000000000000000000, 0.000000000000000000, -1.000000000000000000 ) ) ;
#2221=ORIENTED_EDGE ( 'NONE', *, *, #1401, .F. ) ;
#2231=EDGE_CURVE ( 'NONE', #8785, #1325, #21496, .T. ) ;
#2241=CARTESIAN_POINT ( 'NONE',  ( 2.916637777638891649, -2.156686440539167915, 2.039999999999998703 ) ) ;
#2245=LINE ( 'NONE', #14988, #22212 ) ;
#2246=ORIENTED_EDGE ( 'NONE', *, *, #342, .T. ) ;
#2261=DIRECTION ( 'NONE',  ( -0.000000000000000000, -0.000000000000000000, 1.000000000000000000 ) ) ;
#2277=ADVANCED_FACE ( 'NONE', ( #23399 ), #5857, .T. ) ;
#2278=CARTESIAN_POINT ( 'NONE',  ( 1.432654583217642275, -3.458734124999999882, -0.6999999986344028757 ) ) ;
#2280=CARTESIAN_POINT ( 'NONE',  ( 2.828427124746190735, -2.828427124746189847, 1.675000000000001155 ) ) ;
#2291=CARTESIAN_POINT ( 'NONE',  ( -4.000000000000000000, 0.000000000000000000, 1.425000002731187765 ) ) ;
#2305=DIRECTION ( 'NONE',  ( -0.000000000000000000, -0.000000000000000000, 1.000000000000000000 ) ) ;
#2306=B_SPLINE_CURVE_WITH_KNOTS ( 'NONE', 3,
 ( #18528, #18304, #12934, #10906 ),
 .UNSPECIFIED., .F., .F.,
 ( 4, 4 ),
 ( 0.000000000000000000, 0.1324062220596828598 ),
 .UNSPECIFIED. ) ;
#2308=CARTESIAN_POINT ( 'NONE',  ( -3.458734125000000770, 0.000000000000000000, 4.987500001365595459 ) ) ;
#2314=VERTEX_POINT ( 'NONE', #6363 ) ;
#2318=CARTESIAN_POINT ( 'NONE',  ( 6.353591512924457348E-16, -3.458734125000000326, 2.987500001365597235 ) ) ;
#2320=CARTESIAN_POINT ( 'NONE',  ( -5.434916218090833695, -4.367703157927336655, -0.2578475836320747172 ) ) ;
#2331=CARTESIAN_POINT ( 'NONE',  ( -3.250000000000004441, 5.629165124598849879, -3.700000000000000178 ) ) ;
#2335=CARTESIAN_POINT ( 'NONE',  ( -3.458734125000000326, -1.432654583217642497, 5.050000001365596347 ) ) ;
#2342=CARTESIAN_POINT ( 'NONE',  ( -1.656854249492381248, -3.999999999999999112, 4.612500002731188431 ) ) ;
#2356=ORIENTED_EDGE ( 'NONE', *, *, #16601, .F. ) ;
#2379=CARTESIAN_POINT ( 'NONE',  ( 4.623144047065554041, 4.836380039389420737, -3.593844378834468056 ) ) ;
#2388=CARTESIAN_POINT ( 'NONE',  ( 4.350941807883109469, 4.993536075455421219, -0.06682554136337783002 ) ) ;
#2393=CARTESIAN_POINT ( 'NONE',  ( 3.458734125000001214, -1.432654583217639610, -2.574999998634404541 ) ) ;
#2394=CARTESIAN_POINT ( 'NONE',  ( -2.828427124746189403, -2.828427124746190735, 2.425000000000001599 ) ) ;
#2399=( BOUNDED_CURVE ( )  B_SPLINE_CURVE ( 2, ( #5639, #2150, #18567, #22270, #2032, #20713, #17023, #9728, #4317 ),
 .UNSPECIFIED., .F., .F. ) 
 B_SPLINE_CURVE_WITH_KNOTS ( ( 3, 2, 2, 2, 3 ),
 ( 0.8499999999999999778, 0.8625000000000000444, 0.8750000000000000000, 0.8874999999999999556, 0.9000000000000000222 ),
 .UNSPECIFIED. ) 
 CURVE ( )  GEOMETRIC_REPRESENTATION_ITEM ( )  RATIONAL_B_SPLINE_CURVE ( ( 1.000000000000000000, 0.9238795325112867385, 1.000000000000000000, 0.9238795325112867385, 1.000000000000000000, 0.9238795325112867385, 1.000000000000000000, 0.9238795325112867385, 1.000000000000000000 ) ) 
 REPRESENTATION_ITEM ( '' )  );
#2420=CARTESIAN_POINT ( 'NONE',  ( -1.432654583217641164, -3.458734125000000326, 2.175000001365597679 ) ) ;
#2428=CARTESIAN_POINT ( 'NONE',  ( 1.432654583217642275, -3.458734124999999437, 1.050000001365596791 ) ) ;
#2430=CARTESIAN_POINT ( 'NONE',  ( 3.458734125000000326, 4.235727675282971730E-16, 0.2375000013655967357 ) ) ;
#2438=CARTESIAN_POINT ( 'NONE',  ( -2.445694354108819635, -2.445694354108820967, -1.887499998634403431 ) ) ;
#2441=EDGE_CURVE ( 'NONE', #23104, #9739, #12007, .T. ) ;
#2446=CARTESIAN_POINT ( 'NONE',  ( 6.353591512924457348E-16, -3.458734125000000770, 5.237500001365596347 ) ) ;
#2453=CARTESIAN_POINT ( 'NONE',  ( 1.656854249492380360, 4.000000000000000000, 4.112500002731187543 ) ) ;
#2455=ORIENTED_EDGE ( 'NONE', *, *, #11790, .T. ) ;
#2458=CYLINDRICAL_SURFACE ( 'NONE', #8723, 6.499999999999999112 ) ;
#2479=ORIENTED_EDGE ( 'NONE', *, *, #3099, .F. ) ;
#2480=CARTESIAN_POINT ( 'NONE',  ( -3.251184232703611343, 2.330193357860981695, -3.674599999999999866 ) ) ;
#2492=EDGE_CURVE ( 'NONE', #15511, #10158, #580, .T. ) ;
#2494=CARTESIAN_POINT ( 'NONE',  ( -5.968343123267130679, 4.059728990630802947, -3.296662375310749127 ) ) ;
#2496=CARTESIAN_POINT ( 'NONE',  ( 0.000000000000000000, 0.000000000000000000, 0.000000000000000000 ) ) ;
#2510=CARTESIAN_POINT ( 'NONE',  ( -2.828427124746189403, -2.828427124746190735, -0.5749999999999974021 ) ) ;
#2521=CARTESIAN_POINT ( 'NONE',  ( -2.828427124746190291, 2.828427124746190291, -1.699999997268811569 ) ) ;
#2533=CARTESIAN_POINT ( 'NONE',  ( 3.458734125000001214, -1.432654583217639610, 4.425000001365595459 ) ) ;
#2541=CARTESIAN_POINT ( 'NONE',  ( 2.445694354108820079, 2.445694354108820523, 3.362500001365597679 ) ) ;
#2542=CARTESIAN_POINT ( 'NONE',  ( 2.445694354108820079, 2.445694354108820523, -0.6374999986344040970 ) ) ;
#2548=AXIS2_PLACEMENT_3D ( 'NONE', #12304, #8821, #17785 ) ;
#2550=CARTESIAN_POINT ( 'NONE',  ( 6.353591512924457348E-16, -3.458734125000000770, -1.762499998634403209 ) ) ;
#2558=CARTESIAN_POINT ( 'NONE',  ( -1.432654583217640276, 3.458734125000000326, -3.449999998634403653 ) ) ;
#2562=EDGE_CURVE ( 'NONE', #14122, #19663, #21172, .T. ) ;
#2573=CARTESIAN_POINT ( 'NONE',  ( 4.000000000000000888, -1.656854249492379694, 1.862500002731187765 ) ) ;
#2588=CARTESIAN_POINT ( 'NONE',  ( -0.5316568767328819778, -7.198601258566901251, -3.296662375310746462 ) ) ;
#2604=EDGE_CURVE ( 'NONE', #2635, #12546, #23461, .T. ) ;
#2621=DIRECTION ( 'NONE',  ( -0.000000000000000000, -0.000000000000000000, 1.000000000000000000 ) ) ;
#2629=CARTESIAN_POINT ( 'NONE',  ( -2.449293598294706907E-16, 4.000000000000000000, 3.050000000000002487 ) ) ;
#2635=VERTEX_POINT ( 'NONE', #3578 ) ;
#2649=DIRECTION ( 'NONE',  ( 0.000000000000000000, -1.000000000000000000, 0.000000000000000000 ) ) ;
#2656=CARTESIAN_POINT ( 'NONE',  ( 6.499999999999999112, 0.000000000000000000, 1.734723475976807094E-15 ) ) ;
#2659=CARTESIAN_POINT ( 'NONE',  ( 3.458734125000001214, -1.432654583217639610, 2.425000001365597679 ) ) ;
#2670=CARTESIAN_POINT ( 'NONE',  ( 2.445694354108820523, -2.445694354108820079, 3.112500001365597679 ) ) ;
#2672=CARTESIAN_POINT ( 'NONE',  ( -2.117863837641485618E-16, 3.458734125000000326, -0.5124999986344038749 ) ) ;
#2675=FACE_OUTER_BOUND ( 'NONE', #6603, .T. ) ;
#2684=CARTESIAN_POINT ( 'NONE',  ( 3.458734125000000770, 1.432654583217640498, -2.449999998634404541 ) ) ;
#2692=CARTESIAN_POINT ( 'NONE',  ( -2.445694354108820523, 2.445694354108820523, 5.862500001365596347 ) ) ;
#2700=CARTESIAN_POINT ( 'NONE',  ( 2.828427124746189847, 2.828427124746190291, 3.050000002731189319 ) ) ;
#2706=CYLINDRICAL_SURFACE ( 'NONE', #20963, 4.000000000000000000 ) ;
#2726=DIRECTION ( 'NONE',  ( -1.000000000000000000, 3.552713678800500929E-15, 0.000000000000000000 ) ) ;
#2730=CARTESIAN_POINT ( 'NONE',  ( -6.500000000000000000, 0.000000000000000000, -3.700000000000000178 ) ) ;
#2748=CARTESIAN_POINT ( 'NONE',  ( -2.465616269789157045, 2.433468530533930974, -3.295601554149322876 ) ) ;
#2757=CARTESIAN_POINT ( 'NONE',  ( 4.000000000000000000, 1.656854249492381248, -2.012499997268812013 ) ) ;
#2761=CARTESIAN_POINT ( 'NONE',  ( -4.000000000000000888, 1.656854249492380582, -0.6374999972688124572 ) ) ;
#2773=CARTESIAN_POINT ( 'NONE',  ( -3.458734125000000326, -1.432654583217642497, 5.050000001365596347 ) ) ;
#2782=CARTESIAN_POINT ( 'NONE',  ( 3.458734125000000326, 1.432654583217640498, 2.300000001365597679 ) ) ;
#2783=CARTESIAN_POINT ( 'NONE',  ( 1.432654583217642053, -3.458734124999999437, 0.05000000136559583364 ) ) ;
#2787=VECTOR ( 'NONE', #12767, 1000.000000000000000 ) ;
#2804=AXIS2_PLACEMENT_3D ( 'NONE', #12603, #19864, #20442 ) ;
#2805=CARTESIAN_POINT ( 'NONE',  ( -3.458734125000000770, 0.000000000000000000, 2.987500001365597235 ) ) ;
#2810=FACE_BOUND ( 'NONE', #8956, .T. ) ;
#2813=FACE_OUTER_BOUND ( 'NONE', #21360, .T. ) ;
#2828=CARTESIAN_POINT ( 'NONE',  ( -2.445694354108820523, 2.445694354108820523, 5.612500001365596347 ) ) ;
#2848=DIRECTION ( 'NONE',  ( -0.000000000000000000, -0.000000000000000000, 1.000000000000000000 ) ) ;
#2859=CARTESIAN_POINT ( 'NONE',  ( -4.000000000000000000, 0.000000000000000000, -0.6999999999999975131 ) ) ;
#2862=DIRECTION ( 'NONE',  ( -0.000000000000000000, -0.000000000000000000, 1.000000000000000000 ) ) ;
#2875=CARTESIAN_POINT ( 'NONE',  ( 5.479999999999998650, 0.000000000000000000, 2.039999999999998259 ) ) ;
#2885=CARTESIAN_POINT ( 'NONE',  ( -2.445694354108819635, -2.445694354108820967, 0.1125000013655966247 ) ) ;
#2889=FACE_OUTER_BOUND ( 'NONE', #12909, .T. ) ;
#2897=CARTESIAN_POINT ( 'NONE',  ( 0.5784715375562682338, -3.458734124999999882, 2.012736001390156737 ) ) ;
#2906=CARTESIAN_POINT ( 'NONE',  ( -2.117863837641485618E-16, 3.458734125000000770, -1.262499998634402765 ) ) ;
#2915=CARTESIAN_POINT ( 'NONE',  ( -1.432654583217641164, -3.458734125000000326, 0.1750000013655959585 ) ) ;
#2921=CARTESIAN_POINT ( 'NONE',  ( -2.828427124746190291, 2.828427124746190291, -1.824999999999998401 ) ) ;
#2923=CARTESIAN_POINT ( 'NONE',  ( 4.714285714285714413, 0.000000000000000000, 2.039999999999998259 ) ) ;
#2924=CARTESIAN_POINT ( 'NONE',  ( 2.828427124746189847, 2.828427124746190291, -0.9499999972688126793 ) ) ;
#2941=CARTESIAN_POINT ( 'NONE',  ( -2.445694354108820523, 2.445694354108820523, 4.612500001365595459 ) ) ;
#2952=ORIENTED_EDGE ( 'NONE', *, *, #15835, .F. ) ;
#2975=CARTESIAN_POINT ( 'NONE',  ( 6.499999999999999112, 0.000000000000000000, 1.734723475976807094E-15 ) ) ;
#2977=CARTESIAN_POINT ( 'NONE',  ( -4.000000000000000000, 0.000000000000000000, -2.699999999999999289 ) ) ;
#2987=( BOUNDED_CURVE ( )  B_SPLINE_CURVE ( 2, ( #6364, #6484, #4558, #21173, #19164, #720, #6124, #13452, #4672 ),
 .UNSPECIFIED., .F., .F. ) 
 B_SPLINE_CURVE_WITH_KNOTS ( ( 3, 2, 2, 2, 3 ),
 ( 0.6999999999999999556, 0.7125000000000000222, 0.7249999999999999778, 0.7375000000000000444, 0.7500000000000000000 ),
 .UNSPECIFIED. ) 
 CURVE ( )  GEOMETRIC_REPRESENTATION_ITEM ( )  RATIONAL_B_SPLINE_CURVE ( ( 1.000000000000000000, 0.9238795325112867385, 1.000000000000000000, 0.9238795325112867385, 1.000000000000000000, 0.9238795325112867385, 1.000000000000000000, 0.9238795325112867385, 1.000000000000000000 ) ) 
 REPRESENTATION_ITEM ( '' )  );
#2994=CARTESIAN_POINT ( 'NONE',  ( 4.000000000000000000, 1.656854249492381248, -1.012499997268812901 ) ) ;
#3005=CARTESIAN_POINT ( 'NONE',  ( -2.445694354108819635, -2.445694354108820967, -1.887499998634403431 ) ) ;
#3028=AXIS2_PLACEMENT_3D ( 'NONE', #10356, #6621, #12268 ) ;
#3039=FACE_OUTER_BOUND ( 'NONE', #663, .T. ) ;
#3041=CARTESIAN_POINT ( 'NONE',  ( -3.458734125000000770, 0.000000000000000000, 0.9875000013655956810 ) ) ;
#3053=CARTESIAN_POINT ( 'NONE',  ( 2.828427124746189847, 2.828427124746190291, 2.050000002731188431 ) ) ;
#3073=CARTESIAN_POINT ( 'NONE',  ( 3.458734125000000326, 1.432654583217640498, 4.300000001365595459 ) ) ;
#3080=CARTESIAN_POINT ( 'NONE',  ( -3.502865032392102673, 0.9776794494524829737, 2.039999999999989821 ) ) ;
#3082=CARTESIAN_POINT ( 'NONE',  ( -4.000000000000000000, -1.656854249492383024, -1.637499999999997957 ) ) ;
#3099=EDGE_CURVE ( 'NONE', #11761, #20113, #20430, .T. ) ;
#3108=CARTESIAN_POINT ( 'NONE',  ( -2.449293598294706907E-16, 4.000000000000000000, -0.9499999999999977351 ) ) ;
#3111=CARTESIAN_POINT ( 'NONE',  ( 0.000000000000000000, 0.000000000000000000, 0.000000000000000000 ) ) ;
#3112=B_SPLINE_CURVE_WITH_KNOTS ( 'NONE', 3,
 ( #3548, #18396, #13035, #16374, #10995, #5465 ),
 .UNSPECIFIED., .F., .F.,
 ( 4, 2, 4 ),
 ( 0.006695446894088489739, 0.008593684019695166376, 0.01049192114530184475 ),
 .UNSPECIFIED. ) ;
#3131=CARTESIAN_POINT ( 'NONE',  ( 1.432654583217640276, 3.458734125000000770, -1.324999998634403653 ) ) ;
#3151=CARTESIAN_POINT ( 'NONE',  ( -2.828427124746189403, -2.828427124746190735, -2.449999997268812457 ) ) ;
#3155=CARTESIAN_POINT ( 'NONE',  ( -1.432654583217641164, -3.458734125000000326, 1.175000001365597013 ) ) ;
#3156=CARTESIAN_POINT ( 'NONE',  ( -2.441083172237810572, -2.460707566094265442, 2.039999999999996039 ) ) ;
#3164=CARTESIAN_POINT ( 'NONE',  ( -4.000000000000000888, 1.656854249492380804, -1.637499997268811569 ) ) ;
#3184=CARTESIAN_POINT ( 'NONE',  ( -1.432654583217640942, -3.458734124999999882, 3.925000001365594127 ) ) ;
#3190=CARTESIAN_POINT ( 'NONE',  ( -1.237965327229626045, 3.704993550908596056, 2.039999999999998703 ) ) ;
#3218=CARTESIAN_POINT ( 'NONE',  ( 2.828427124746190735, -2.828427124746189847, -2.324999999999998845 ) ) ;
#3225=CARTESIAN_POINT ( 'NONE',  ( 6.353591512924457348E-16, -3.458734125000000326, -3.012499998634404541 ) ) ;
#3227=AXIS2_PLACEMENT_3D ( 'NONE', #9882, #22550, #13480 ) ;
#3247=CARTESIAN_POINT ( 'NONE',  ( 3.458734125000001214, -1.432654583217639610, 1.425000001365596791 ) ) ;
#3258=CARTESIAN_POINT ( 'NONE',  ( -1.432654583217640276, 3.458734125000000326, -2.449999998634404541 ) ) ;
#3275=CARTESIAN_POINT ( 'NONE',  ( 2.828427124746190735, -2.828427124746189847, -2.199999997268812013 ) ) ;
#3280=CARTESIAN_POINT ( 'NONE',  ( -3.458734125000000326, -1.432654583217642497, 0.05000000136559582670 ) ) ;
#3281=CARTESIAN_POINT ( 'NONE',  ( -3.196266448073070254, -1.341181843264293905, 2.040000000000002256 ) ) ;
#3289=CARTESIAN_POINT ( 'NONE',  ( -1.656854249492380804, 4.000000000000000000, -1.762499997268811569 ) ) ;
#3305=CARTESIAN_POINT ( 'NONE',  ( -2.117863837641485618E-16, 3.458734125000000326, 4.487500001365595459 ) ) ;
#3311=CARTESIAN_POINT ( 'NONE',  ( -3.429173157536499428, 1.281533049792265677, 2.039999999999997371 ) ) ;
#3312=CARTESIAN_POINT ( 'NONE',  ( -6.499999999999999112, 3.145973671264225668, -3.294612376748628613 ) ) ;
#3318=ORIENTED_EDGE ( 'NONE', *, *, #5565, .T. ) ;
#3324=DIRECTION ( 'NONE',  ( -1.000000000000000000, 0.000000000000000000, 0.000000000000000000 ) ) ;
#3345=EDGE_CURVE ( 'NONE', #15758, #16269, #14961, .T. ) ;
#3348=CARTESIAN_POINT ( 'NONE',  ( -1.432654583217640942, -3.458734124999999882, -3.074999998634404541 ) ) ;
#3366=CARTESIAN_POINT ( 'NONE',  ( 3.458734125000001214, -1.432654583217639610, 0.4250000013655961251 ) ) ;
#3392=CARTESIAN_POINT ( 'NONE',  ( 7.347880794884118750E-16, -4.000000000000000000, -2.324999997268812013 ) ) ;
#3396=CARTESIAN_POINT ( 'NONE',  ( 2.445694354108820967, -2.445694354108820079, -2.637499998634404097 ) ) ;
#3408=CARTESIAN_POINT ( 'NONE',  ( 7.347880794884118750E-16, -4.000000000000000000, 1.675000002731187987 ) ) ;
#3409=DIRECTION ( 'NONE',  ( -0.5000000000000006661, 0.8660254037844383745, 0.000000000000000000 ) ) ;
#3416=CARTESIAN_POINT ( 'NONE',  ( 2.828427124746189847, 2.828427124746190291, -2.949999997268812901 ) ) ;
#3420=( BOUNDED_CURVE ( )  B_SPLINE_CURVE ( 2, ( #10724, #20330, #5859, #3822, #9598 ),
 .UNSPECIFIED., .F., .F. ) 
 B_SPLINE_CURVE_WITH_KNOTS ( ( 3, 2, 3 ),
 ( 0.9000000000000000222, 0.9124999999999999778, 0.9250000000000000444 ),
 .UNSPECIFIED. ) 
 CURVE ( )  GEOMETRIC_REPRESENTATION_ITEM ( )  RATIONAL_B_SPLINE_CURVE ( ( 1.000000000000000000, 0.9238795325112867385, 1.000000000000000000, 0.9238795325112867385, 1.000000000000000000 ) ) 
 REPRESENTATION_ITEM ( '' )  );
#3422=CONICAL_SURFACE ( 'NONE', #17195, 6.500000000000000888, 1.047197551196596521 ) ;
#3430=CARTESIAN_POINT ( 'NONE',  ( 6.353591512924457348E-16, -3.458734125000000326, -0.01249999863440348635 ) ) ;
#3436=CARTESIAN_POINT ( 'NONE',  ( -3.478414791966562891, -0.5482830432473079219, 2.039999999999999591 ) ) ;
#3445=CARTESIAN_POINT ( 'NONE',  ( -6.499999999999999112, -0.6341575537611441327, 4.540096597283048831E-16 ) ) ;
#3454=DIRECTION ( 'NONE',  ( 1.000000000000000000, 0.000000000000000000, 0.000000000000000000 ) ) ;
#3459=CARTESIAN_POINT ( 'NONE',  ( -4.000000000000000000, 0.000000000000000000, 0.3000000000000016542 ) ) ;
#3465=CARTESIAN_POINT ( 'NONE',  ( -1.338706173739542260, 3.195114087442786577, -3.295601554149324652 ) ) ;
#3467=CARTESIAN_POINT ( 'NONE',  ( -1.656854249492381248, -3.999999999999999112, 0.6125000027311866546 ) ) ;
#3471=CARTESIAN_POINT ( 'NONE',  ( -2.445694354108819635, -2.445694354108820523, -3.137499998634404541 ) ) ;
#3475=EDGE_LOOP ( 'NONE', ( #17479, #16631, #2109, #7654 ) ) ;
#3490=CARTESIAN_POINT ( 'NONE',  ( -2.828427124746189403, -2.828427124746190735, 4.424999999999999822 ) ) ;
#3502=CARTESIAN_POINT ( 'NONE',  ( 2.445694354108820523, -2.445694354108820079, -2.887499998634404097 ) ) ;
#3518=CARTESIAN_POINT ( 'NONE',  ( -4.000000000000000000, 0.000000000000000000, -2.699999999999999289 ) ) ;
#3526=CARTESIAN_POINT ( 'NONE',  ( -4.000000000000000888, 1.656854249492380804, -2.637499997268812013 ) ) ;
#3532=EDGE_CURVE ( 'NONE', #15758, #14307, #13162, .T. ) ;
#3533=CARTESIAN_POINT ( 'NONE',  ( 4.000000000000000000, 4.898587196589412829E-16, 0.8000000000000020428 ) ) ;
#3538=EDGE_CURVE ( 'NONE', #10786, #10158, #16412, .T. ) ;
#3540=CARTESIAN_POINT ( 'NONE',  ( -2.974182810908594821, 5.788408252967899514, -3.700000000000004174 ) ) ;
#3543=CARTESIAN_POINT ( 'NONE',  ( -1.432654583217640942, -3.458734124999999882, -1.074999998634403209 ) ) ;
#3548=CARTESIAN_POINT ( 'NONE',  ( 6.499999999999999112, -3.752776749732574135, -3.119443416399232394 ) ) ;
#3553=CARTESIAN_POINT ( 'NONE',  ( -4.000000000000000000, 0.000000000000000000, -1.574999997268811569 ) ) ;
#3555=ORIENTED_EDGE ( 'NONE', *, *, #14408, .T. ) ;
#3560=VECTOR ( 'NONE', #2862, 1000.000000000000000 ) ;
#3578=CARTESIAN_POINT ( 'NONE',  ( -4.714285714285714413, 5.773334910266094008E-16, 2.039999999999998259 ) ) ;
#3582=CARTESIAN_POINT ( 'NONE',  ( -2.117863837641485618E-16, 3.458734125000000326, -2.512499998634404097 ) ) ;
#3598=CARTESIAN_POINT ( 'NONE',  ( 4.000000000000000000, 4.898587196589412829E-16, 3.800000000000002931 ) ) ;
#3610=VERTEX_POINT ( 'NONE', #11387 ) ;
#3627=EDGE_LOOP ( 'NONE', ( #6368, #3964, #20949 ) ) ;
#3633=CARTESIAN_POINT ( 'NONE',  ( -2.445694354108819635, -2.445694354108820523, 4.862500001365595459 ) ) ;
#3639=CARTESIAN_POINT ( 'NONE',  ( -2.449293598294706907E-16, 4.000000000000000000, -2.949999999999997957 ) ) ;
#3645=AXIS2_PLACEMENT_3D ( 'NONE', #22187, #3878, #49 ) ;
#3653=CARTESIAN_POINT ( 'NONE',  ( -1.432654583217640276, 3.458734125000000326, -0.4499999986344046521 ) ) ;
#3675=CARTESIAN_POINT ( 'NONE',  ( -1.656854249492381248, -3.999999999999999112, -0.5124999999999968470 ) ) ;
#3678=CARTESIAN_POINT ( 'NONE',  ( -2.117863837641485618E-16, 3.458734125000000770, -3.262499998634402765 ) ) ;
#3680=CARTESIAN_POINT ( 'NONE',  ( 1.125461230421587633, -3.270501301980698550, 2.040000000000001812 ) ) ;
#3692=CARTESIAN_POINT ( 'NONE',  ( -3.458734124999999882, -1.432654583217642497, -3.199999998634404985 ) ) ;
#3702=CYLINDRICAL_SURFACE ( 'NONE', #12971, 4.000000000000000000 ) ;
#3707=CARTESIAN_POINT ( 'NONE',  ( 3.250000000000004441, 5.629165124598849879, -3.700000000000000178 ) ) ;
#3711=CARTESIAN_POINT ( 'NONE',  ( -2.117863837641485618E-16, 3.458734125000000770, -2.262499998634403653 ) ) ;
#3715=ORIENTED_EDGE ( 'NONE', *, *, #10558, .F. ) ;
#3722=CARTESIAN_POINT ( 'NONE',  ( -4.000000000000000888, 1.656854249492380582, 1.362500002731187321 ) ) ;
#3735=DIRECTION ( 'NONE',  ( 0.8660254037844383745, 0.5000000000000004441, 0.000000000000000000 ) ) ;
#3748=CARTESIAN_POINT ( 'NONE',  ( -3.458734124999999882, -1.432654583217642497, 4.800000001365595459 ) ) ;
#3749=CARTESIAN_POINT ( 'NONE',  ( -6.500000000000000000, -3.752776749732573247, -0.5805565836007695601 ) ) ;
#3763=CARTESIAN_POINT ( 'NONE',  ( -1.432654583217640498, 3.458734125000000770, 0.8000000013655964581 ) ) ;
#3771=CARTESIAN_POINT ( 'NONE',  ( -2.117863837641485618E-16, 3.458734125000000326, 1.487500001365596125 ) ) ;
#3780=ORIENTED_EDGE ( 'NONE', *, *, #2231, .F. ) ;
#3782=FACE_OUTER_BOUND ( 'NONE', #15118, .T. ) ;
#3785=VERTEX_POINT ( 'NONE', #6338 ) ;
#3796=PRODUCT_DEFINITION_FORMATION_WITH_SPECIFIED_SOURCE ( 'ANY', '', #12046, .NOT_KNOWN. ) ;
#3813=ORIENTED_EDGE ( 'NONE', *, *, #17425, .F. ) ;
#3822=CARTESIAN_POINT ( 'NONE',  ( -1.656854249492380582, 4.000000000000000000, -2.887499999999997069 ) ) ;
#3826=CARTESIAN_POINT ( 'NONE',  ( 2.828427124746190735, -2.828427124746189847, 1.675000000000001155 ) ) ;
#3843=CARTESIAN_POINT ( 'NONE',  ( 6.353591512924457348E-16, -3.458734125000000770, -2.762499998634404097 ) ) ;
#3856=CIRCLE ( 'NONE', #11923, 6.500000000000000888 ) ;
#3876=SURFACE_STYLE_USAGE ( .BOTH. , #13007 ) ;
#3877=CARTESIAN_POINT ( 'NONE',  ( 3.458734125000000326, 4.235727675282971730E-16, 4.237500001365595459 ) ) ;
#3878=DIRECTION ( 'NONE',  ( -0.000000000000000000, -0.000000000000000000, 1.000000000000000000 ) ) ;
#3881=CARTESIAN_POINT ( 'NONE',  ( 7.347880794884118750E-16, -4.000000000000000000, -2.449999999999998845 ) ) ;
#3885=CARTESIAN_POINT ( 'NONE',  ( 3.458734125000000770, 4.235727675282972223E-16, 0.4875000013655969577 ) ) ;
#3890=CARTESIAN_POINT ( 'NONE',  ( -2.445694354108820523, 2.445694354108820523, -0.3874999986344038194 ) ) ;
#3917=CARTESIAN_POINT ( 'NONE',  ( 6.499999999999999112, 0.000000000000000000, 2.040000000000001812 ) ) ;
#3931=CARTESIAN_POINT ( 'NONE',  ( -6.500000000000000000, 3.752776749732564809, -0.5805565836007661185 ) ) ;
#3940=CARTESIAN_POINT ( 'NONE',  ( -2.828427124746189403, -2.828427124746190735, 1.425000000000000933 ) ) ;
#3942=CARTESIAN_POINT ( 'NONE',  ( -5.432802636760778014, 4.368923434677190798, -3.442664554191217530 ) ) ;
#3948=AXIS2_PLACEMENT_3D ( 'NONE', #10802, #7430, #7193 ) ;
#3956=CARTESIAN_POINT ( 'NONE',  ( -1.432654583217641164, -3.458734125000000326, -2.824999998634404985 ) ) ;
#3957=CARTESIAN_POINT ( 'NONE',  ( -2.828427124746190291, 2.828427124746190291, 4.174999999999999822 ) ) ;
#3964=ORIENTED_EDGE ( 'NONE', *, *, #21194, .F. ) ;
#3980=CARTESIAN_POINT ( 'NONE',  ( -5.007715329123867711E-16, -7.505553499465146494, -3.700000000000000178 ) ) ;
#3983=CARTESIAN_POINT ( 'NONE',  ( -1.432654583217640498, 3.458734125000000770, 5.800000001365597235 ) ) ;
#3993=CARTESIAN_POINT ( 'NONE',  ( 6.353591512924457348E-16, -3.458734125000000326, 4.987500001365595459 ) ) ;
#4008=CARTESIAN_POINT ( 'NONE',  ( -4.000000000000000000, 4.898587196589412829E-16, 19.04999999999996874 ) ) ;
#4013=CARTESIAN_POINT ( 'NONE',  ( 1.432654583217639832, 3.458734125000000326, -2.574999998634404541 ) ) ;
#4026=B_SPLINE_CURVE_WITH_KNOTS ( 'NONE', 3,
 ( #12248, #19516, #17734, #15937, #2127, #18198 ),
 .UNSPECIFIED., .F., .F.,
 ( 4, 2, 4 ),
 ( 2.380733003149298079E-07, 0.001898835937927375499, 0.003797433802554436334 ),
 .UNSPECIFIED. ) ;
#4044=CARTESIAN_POINT ( 'NONE',  ( 3.602667665204950076, -0.9740173600655226416, 2.039999999999998703 ) ) ;
#4065=CYLINDRICAL_SURFACE ( 'NONE', #9942, 4.000000000000000000 ) ;
#4076=CARTESIAN_POINT ( 'NONE',  ( 3.458734125000000770, 4.235727675282972223E-16, -1.512499998634402987 ) ) ;
#4077=CARTESIAN_POINT ( 'NONE',  ( 1.656854249492383024, -3.999999999999999112, 2.612500000000002043 ) ) ;
#4081=VERTEX_POINT ( 'NONE', #3917 ) ;
#4087=CARTESIAN_POINT ( 'NONE',  ( 4.000000000000000000, 1.656854249492381248, 0.9875000027311868767 ) ) ;
#4105=CARTESIAN_POINT ( 'NONE',  ( -1.432654583217640498, 3.458734125000000770, 3.800000001365595459 ) ) ;
#4114=CARTESIAN_POINT ( 'NONE',  ( -3.458734124999999882, -1.432654583217642497, 3.800000001365595459 ) ) ;
#4122=CARTESIAN_POINT ( 'NONE',  ( 3.458734125000001214, -1.432654583217639610, -0.5749999986344027647 ) ) ;
#4125=CARTESIAN_POINT ( 'NONE',  ( 4.000000000000000000, 4.898587196589412829E-16, -1.074999997268812679 ) ) ;
#4133=CARTESIAN_POINT ( 'NONE',  ( -2.445694354108819635, -2.445694354108820523, -3.137499998634404541 ) ) ;
#4167=ORIENTED_EDGE ( 'NONE', *, *, #17014, .F. ) ;
#4178=CARTESIAN_POINT ( 'NONE',  ( 2.149474931388133836, 6.264553569211845918, -0.05533025579362121221 ) ) ;
#4182=CARTESIAN_POINT ( 'NONE',  ( 0.000000000000000000, 0.000000000000000000, 19.04999999999996874 ) ) ;
#4187=( BOUNDED_CURVE ( )  B_SPLINE_CURVE ( 2, ( #21522, #12113, #19733, #6701, #15819, #23091, #17952, #14016, #4900 ),
 .UNSPECIFIED., .F., .F. ) 
 B_SPLINE_CURVE_WITH_KNOTS ( ( 3, 2, 2, 2, 3 ),
 ( 0.6500000000000000222, 0.6624999999999999778, 0.6750000000000000444, 0.6875000000000000000, 0.6999999999999999556 ),
 .UNSPECIFIED. ) 
 CURVE ( )  GEOMETRIC_REPRESENTATION_ITEM ( )  RATIONAL_B_SPLINE_CURVE ( ( 1.000000000000000000, 0.9238795325112867385, 1.000000000000000000, 0.9238795325112867385, 1.000000000000000000, 0.9238795325112867385, 1.000000000000000000, 0.9238795325112867385, 1.000000000000000000 ) ) 
 REPRESENTATION_ITEM ( '' )  );
#4198=CARTESIAN_POINT ( 'NONE',  ( -2.117863837641485618E-16, 3.458734125000000770, -1.262499998634402765 ) ) ;
#4200=CARTESIAN_POINT ( 'NONE',  ( -4.000000000000000888, 1.656854249492380804, 2.237500000000001599 ) ) ;
#4228=CARTESIAN_POINT ( 'NONE',  ( 1.432654583217640276, 3.458734125000000770, 2.675000001365597679 ) ) ;
#4238=FILL_AREA_STYLE ('',( #13243 ) ) ;
#4240=CARTESIAN_POINT ( 'NONE',  ( -3.458734125000000326, 0.000000000000000000, 3.737500001365594571 ) ) ;
#4243=ORIENTED_EDGE ( 'NONE', *, *, #5123, .F. ) ;
#4253=LINE ( 'NONE', #22566, #12224 ) ;
#4258=CARTESIAN_POINT ( 'NONE',  ( -2.445694354108819635, -2.445694354108820967, 4.112500001365594571 ) ) ;
#4262=CARTESIAN_POINT ( 'NONE',  ( 4.000000000000000000, 4.898587196589412829E-16, -2.199999999999998845 ) ) ;
#4287=CARTESIAN_POINT ( 'NONE',  ( -2.828427124746189403, -2.828427124746190735, 0.4250000000000017653 ) ) ;
#4302=ORIENTED_EDGE ( 'NONE', *, *, #15990, .F. ) ;
#4306=VERTEX_POINT ( 'NONE', #5347 ) ;
#4316=CARTESIAN_POINT ( 'NONE',  ( 1.656854249492380360, 4.000000000000000000, 2.987500000000002487 ) ) ;
#4317=CARTESIAN_POINT ( 'NONE',  ( -4.000000000000000000, 0.000000000000000000, -3.574999997268813345 ) ) ;
#4337=CARTESIAN_POINT ( 'NONE',  ( 3.250000000000002665, -5.629165124598850767, -3.700000000000000178 ) ) ;
#4340=CARTESIAN_POINT ( 'NONE',  ( 3.458734125000001214, -1.432654583217639610, 5.425000001365595459 ) ) ;
#4351=CARTESIAN_POINT ( 'NONE',  ( 2.445694354108820523, -2.445694354108820079, 1.112500001365595681 ) ) ;
#4352=CARTESIAN_POINT ( 'NONE',  ( -3.458734125000000326, 0.000000000000000000, 0.7375000013655954589 ) ) ;
#4355=PRESENTATION_STYLE_ASSIGNMENT (( #13598 ) ) ;
#4360=CARTESIAN_POINT ( 'NONE',  ( 2.445694354108820079, 2.445694354108820523, -2.387499998634403653 ) ) ;
#4369=CARTESIAN_POINT ( 'NONE',  ( 1.432654583217640276, 3.458734125000000770, 3.675000001365597235 ) ) ;
#4379=CARTESIAN_POINT ( 'NONE',  ( -4.000000000000000888, 1.656854249492380804, 4.362500002731187543 ) ) ;
#4405=CARTESIAN_POINT ( 'NONE',  ( 4.000000000000000000, 4.898587196589412829E-16, 1.925000002731188209 ) ) ;
#4407=ORIENTED_EDGE ( 'NONE', *, *, #14868, .T. ) ;
#4436=CARTESIAN_POINT ( 'NONE',  ( -2.828427124746190291, 2.828427124746190291, 1.175000000000000711 ) ) ;
#4457=CARTESIAN_POINT ( 'NONE',  ( -1.432654583217640498, 3.458734125000000770, 2.800000001365598123 ) ) ;
#4466=CARTESIAN_POINT ( 'NONE',  ( 3.458734125000000326, 1.432654583217640498, 3.300000001365598568 ) ) ;
#4467=CARTESIAN_POINT ( 'NONE',  ( 1.432654583217639832, 3.458734125000000326, -0.5749999986344047631 ) ) ;
#4472=CARTESIAN_POINT ( 'NONE',  ( -6.500000000000000000, -3.752776749732573247, -3.119443416399232394 ) ) ;
#4475=CARTESIAN_POINT ( 'NONE',  ( -1.432654583217640498, 3.458734125000000770, -1.199999998634403209 ) ) ;
#4485=CARTESIAN_POINT ( 'NONE',  ( -1.432654583217640498, 3.458734125000000770, 5.800000001365597235 ) ) ;
#4494=CARTESIAN_POINT ( 'NONE',  ( -2.828427124746189403, -2.828427124746190735, 3.550000002731189763 ) ) ;
#4499=CARTESIAN_POINT ( 'NONE',  ( -1.656854249492381248, -3.999999999999999112, 1.612500002731187543 ) ) ;
#4509=TOROIDAL_SURFACE ( 'NONE', #9506, 5.479999999999998650, 1.020000000000000018 ) ;
#4521=ORIENTED_EDGE ( 'NONE', *, *, #16060, .F. ) ;
#4546=ORIENTED_EDGE ( 'NONE', *, *, #16601, .T. ) ;
#4551=DIRECTION ( 'NONE',  ( -0.000000000000000000, -0.000000000000000000, 1.000000000000000000 ) ) ;
#4555=CARTESIAN_POINT ( 'NONE',  ( 4.000000000000000000, 1.656854249492381248, 0.8625000000000004885 ) ) ;
#4558=CARTESIAN_POINT ( 'NONE',  ( -2.828427124746190291, 2.828427124746190291, -0.8249999999999976241 ) ) ;
#4583=CARTESIAN_POINT ( 'NONE',  ( 3.458734125000000770, 1.432654583217640498, 5.550000001365596347 ) ) ;
#4593=CARTESIAN_POINT ( 'NONE',  ( 3.458734125000000770, -1.432654583217639610, 2.175000001365597679 ) ) ;
#4594=CARTESIAN_POINT ( 'NONE',  ( 1.125461230421587633, -3.270501301980698550, 2.040000000000001812 ) ) ;
#4602=ORIENTED_EDGE ( 'NONE', *, *, #5326, .F. ) ;
#4616=CARTESIAN_POINT ( 'NONE',  ( 1.432654583217642275, -3.458734124999999882, 3.300000001365598568 ) ) ;
#4624=CARTESIAN_POINT ( 'NONE',  ( -2.828427124746190291, 2.828427124746190291, 3.300000002731189319 ) ) ;
#4626=VERTEX_POINT ( 'NONE', #5050 ) ;
#4642=ORIENTED_EDGE ( 'NONE', *, *, #23438, .F. ) ;
#4669=CARTESIAN_POINT ( 'NONE',  ( 4.000000000000000000, 1.656854249492381248, -1.137499999999997513 ) ) ;
#4672=CARTESIAN_POINT ( 'NONE',  ( 4.000000000000000000, 4.898587196589412829E-16, -1.199999999999997957 ) ) ;
#4676=DIRECTION ( 'NONE',  ( -1.000000000000000000, -6.123233995736827666E-17, 0.000000000000000000 ) ) ;
#4682=ORIENTED_EDGE ( 'NONE', *, *, #21627, .T. ) ;
#4687=EDGE_CURVE ( 'NONE', #19427, #19833, #2399, .T. ) ;
#4691=B_SPLINE_CURVE_WITH_KNOTS ( 'NONE', 3,
 ( #22847, #15583, #18904, #6460, #2379, #10071, #15461, #17361 ),
 .UNSPECIFIED., .F., .F.,
 ( 4, 2, 2, 4 ),
 ( 0.003797433802554448044, 0.004743183970586243095, 0.005688934138618039447, 0.007580434474681627816 ),
 .UNSPECIFIED. ) ;
#4693=CARTESIAN_POINT ( 'NONE',  ( -4.000000000000000000, 0.000000000000000000, 0.4250000027311868211 ) ) ;
#4696=CARTESIAN_POINT ( 'NONE',  ( -1.432654583217641164, -3.458734125000000326, 1.175000001365597013 ) ) ;
#4708=CARTESIAN_POINT ( 'NONE',  ( 2.445694354108820079, 2.445694354108820523, 1.362500001365595903 ) ) ;
#4728=CARTESIAN_POINT ( 'NONE',  ( 1.432654583217640276, 3.458734125000000770, 2.675000001365597679 ) ) ;
#4739=CARTESIAN_POINT ( 'NONE',  ( -2.828427124746189403, -2.828427124746190735, 2.550000002731188875 ) ) ;
#4744=ORIENTED_EDGE ( 'NONE', *, *, #8502, .T. ) ;
#4748=DIRECTION ( 'NONE',  ( -0.000000000000000000, -0.000000000000000000, 1.000000000000000000 ) ) ;
#4749=DIRECTION ( 'NONE',  ( 1.000000000000000000, 0.000000000000000000, 0.000000000000000000 ) ) ;
#4751=CARTESIAN_POINT ( 'NONE',  ( -2.117863837641485618E-16, 3.458734125000000326, 2.487500001365596791 ) ) ;
#4755=ORIENTED_EDGE ( 'NONE', *, *, #8201, .F. ) ;
#4765=DIRECTION ( 'NONE',  ( -0.000000000000000000, -0.000000000000000000, 1.000000000000000000 ) ) ;
#4770=CONICAL_SURFACE ( 'NONE', #21190, 6.500000000000000888, 1.047197551196596521 ) ;
#4772=CARTESIAN_POINT ( 'NONE',  ( -3.803704290982251823, 5.309483803148794756, 4.394406930355310159E-15 ) ) ;
#4779=DIRECTION ( 'NONE',  ( -0.000000000000000000, -0.000000000000000000, 1.000000000000000000 ) ) ;
#4781=CARTESIAN_POINT ( 'NONE',  ( 6.500000000000000000, 3.752776749732573247, -0.5805565836007695601 ) ) ;
#4783=CARTESIAN_POINT ( 'NONE',  ( 1.656854249492383024, -3.999999999999999112, -2.387499999999998401 ) ) ;
#4809=( BOUNDED_CURVE ( )  B_SPLINE_CURVE ( 2, ( #14809, #18606, #20511, #11455, #1955 ),
 .UNSPECIFIED., .F., .F. ) 
 B_SPLINE_CURVE_WITH_KNOTS ( ( 3, 2, 3 ),
 ( 0.4260621439306495062, 0.4375000000000000000, 0.4500000000000000111 ),
 .UNSPECIFIED. ) 
 CURVE ( )  GEOMETRIC_REPRESENTATION_ITEM ( )  RATIONAL_B_SPLINE_CURVE ( ( 0.9881630608388305426, 0.9303476039145940346, 1.000000000000000000, 0.9238795325112867385, 1.000000000000000000 ) ) 
 REPRESENTATION_ITEM ( '' )  );
#4810=CARTESIAN_POINT ( 'NONE',  ( 2.445694354108820967, -2.445694354108820079, -1.637499998634403209 ) ) ;
#4814=CARTESIAN_POINT ( 'NONE',  ( 0.000000000000000000, 4.714285714285714413, 3.059999999999998277 ) ) ;
#4821=CARTESIAN_POINT ( 'NONE',  ( 3.458734125000001214, -1.432654583217639610, 1.175000001365597013 ) ) ;
#4823=CARTESIAN_POINT ( 'NONE',  ( 6.500000000000000000, 3.752776749732573247, -0.5805565836007695601 ) ) ;
#4840=CARTESIAN_POINT ( 'NONE',  ( 1.432654583217640276, 3.458734125000000770, -0.3249999986344045411 ) ) ;
#4849=CARTESIAN_POINT ( 'NONE',  ( -2.828427124746190291, 2.828427124746190291, 0.3000000027311867101 ) ) ;
#4869=CARTESIAN_POINT ( 'NONE',  ( -3.458734125000000326, 1.432654583217640276, 2.675000001365597679 ) ) ;
#4893=CARTESIAN_POINT ( 'NONE',  ( 6.500000000000000000, 3.145973671264227889, -3.294612376748629057 ) ) ;
#4900=CARTESIAN_POINT ( 'NONE',  ( -4.000000000000000000, 0.000000000000000000, -1.574999997268811569 ) ) ;
#4905=CARTESIAN_POINT ( 'NONE',  ( 0.000000000000000000, 0.000000000000000000, 2.039999999999998259 ) ) ;
#4919=ORIENTED_EDGE ( 'NONE', *, *, #4687, .F. ) ;
#4926=CIRCLE ( 'NONE', #20591, 6.499999999999999112 ) ;
#4932=CARTESIAN_POINT ( 'NONE',  ( 3.458734125000000770, 1.432654583217640498, 1.550000001365597013 ) ) ;
#4948=CIRCLE ( 'NONE', #13382, 6.500000000000000888 ) ;
#4960=CARTESIAN_POINT ( 'NONE',  ( 4.000000000000000000, 4.898587196589412829E-16, -2.074999997268812013 ) ) ;
#4968=CARTESIAN_POINT ( 'NONE',  ( -2.445694354108820523, 2.445694354108820523, 0.8625000013655955700 ) ) ;
#4976=CARTESIAN_POINT ( 'NONE',  ( -4.000000000000000000, -1.656854249492383246, -1.512499997268811347 ) ) ;
#4981=CARTESIAN_POINT ( 'NONE',  ( 1.065083781909167415, -6.890627091270381754, -0.2578475836320779924 ) ) ;
#4997=CARTESIAN_POINT ( 'NONE',  ( 2.445694354108820523, -2.445694354108820079, 5.112500001365595459 ) ) ;
#5028=CARTESIAN_POINT ( 'NONE',  ( -2.828427124746190291, 2.828427124746190291, -1.824999999999998401 ) ) ;
#5034=CARTESIAN_POINT ( 'NONE',  ( 1.432654583217639832, 3.458734125000000326, -0.5749999986344046521 ) ) ;
#5039=PLANE ( 'NONE',  #9894 ) ;
#5048=CARTESIAN_POINT ( 'NONE',  ( 1.432654583217640276, 3.458734125000000770, 0.6750000013655963471 ) ) ;
#5050=CARTESIAN_POINT ( 'NONE',  ( -3.251184232703611343, 2.330193357860981251, -3.674599999999999866 ) ) ;
#5059=CARTESIAN_POINT ( 'NONE',  ( -3.458734125000000326, 0.000000000000000000, -3.262499998634404541 ) ) ;
#5077=CARTESIAN_POINT ( 'NONE',  ( 3.458734125000000770, 4.235727675282972223E-16, 1.487500001365596125 ) ) ;
#5084=CARTESIAN_POINT ( 'NONE',  ( 1.656854249492380360, 4.000000000000000000, 2.112500002731187987 ) ) ;
#5092=EDGE_CURVE ( 'NONE', #19833, #4626, #14138, .T. ) ;
#5093=FACE_OUTER_BOUND ( 'NONE', #18401, .T. ) ;
#5105=CARTESIAN_POINT ( 'NONE',  ( 1.432654583217642275, -3.458734124999999437, 2.050000001365597679 ) ) ;
#5110=ORIENTED_EDGE ( 'NONE', *, *, #14868, .F. ) ;
#5111=CARTESIAN_POINT ( 'NONE',  ( -3.270501301980698550, -1.125461230421587633, 2.040000000000001812 ) ) ;
#5113=CARTESIAN_POINT ( 'NONE',  ( -2.828427124746189403, -2.828427124746190735, -1.574999999999998179 ) ) ;
#5120=CARTESIAN_POINT ( 'NONE',  ( 4.000000000000000000, 0.000000000000000000, -3.699999999999998401 ) ) ;
#5123=EDGE_CURVE ( 'NONE', #9522, #7689, #959, .T. ) ;
#5139=CARTESIAN_POINT ( 'NONE',  ( 2.828427124746189847, 2.828427124746190291, -2.074999999999998845 ) ) ;
#5142=VERTEX_POINT ( 'NONE', #22719 ) ;
#5144=CARTESIAN_POINT ( 'NONE',  ( 1.432654583217639832, 3.458734125000000326, -2.574999998634404541 ) ) ;
#5151=ORIENTED_EDGE ( 'NONE', *, *, #7527, .T. ) ;
#5153=DIRECTION ( 'NONE',  ( 0.000000000000000000, -0.000000000000000000, 1.000000000000000000 ) ) ;
#5162=DIRECTION ( 'NONE',  ( -0.000000000000000000, -0.000000000000000000, 1.000000000000000000 ) ) ;
#5164=CARTESIAN_POINT ( 'NONE',  ( -2.117863837641485618E-16, 3.458734125000000770, -0.2624999986344037084 ) ) ;
#5181=ORIENTED_EDGE ( 'NONE', *, *, #6695, .T. ) ;
#5194=CARTESIAN_POINT ( 'NONE',  ( 6.353591512924457348E-16, -3.458734125000000770, -0.7624999986344024316 ) ) ;
#5204=CARTESIAN_POINT ( 'NONE',  ( -4.000000000000000000, 0.000000000000000000, 1.425000002731187765 ) ) ;
#5205=PLANE ( 'NONE',  #6318 ) ;
#5209=CARTESIAN_POINT ( 'NONE',  ( 2.149058192116893196, -6.264794173742287420, -0.06682554136338376971 ) ) ;
#5219=CARTESIAN_POINT ( 'NONE',  ( 1.432654583217642275, -3.458734124999999437, 3.050000001365598568 ) ) ;
#5226=CARTESIAN_POINT ( 'NONE',  ( -3.394711121928224884, -0.8419189903391639529, 2.040000000000001368 ) ) ;
#5237=AXIS2_PLACEMENT_3D ( 'NONE', #7022, #19817, #12429 ) ;
#5264=CARTESIAN_POINT ( 'NONE',  ( -1.432654583217640276, 3.458734125000000326, -1.449999998634403653 ) ) ;
#5266=EDGE_CURVE ( 'NONE', #10129, #18029, #11343, .T. ) ;
#5276=DIRECTION ( 'NONE',  ( -0.000000000000000000, -0.000000000000000000, 1.000000000000000000 ) ) ;
#5284=CARTESIAN_POINT ( 'NONE',  ( 2.828427124746189847, 2.828427124746190291, 4.925000000000000711 ) ) ;
#5299=CARTESIAN_POINT ( 'NONE',  ( 6.353591512924457348E-16, -3.458734125000000326, -3.012499998634404541 ) ) ;
#5315=CARTESIAN_POINT ( 'NONE',  ( 3.458734125000000770, 1.432654583217640498, -2.449999998634404097 ) ) ;
#5317=AXIS2_PLACEMENT_3D ( 'NONE', #15592, #2621, #15237 ) ;
#5325=CARTESIAN_POINT ( 'NONE',  ( 2.828427124746189847, 2.828427124746190291, 1.050000002731187321 ) ) ;
#5326=EDGE_CURVE ( 'NONE', #21232, #11906, #8319, .T. ) ;
#5327=CARTESIAN_POINT ( 'NONE',  ( 4.332341089154587834E-16, 7.505553499465137612, -3.700000000000000178 ) ) ;
#5334=CARTESIAN_POINT ( 'NONE',  ( -1.656854249492380582, 4.000000000000000000, -2.762499997268812457 ) ) ;
#5345=CARTESIAN_POINT ( 'NONE',  ( 3.458734125000000326, 1.432654583217640498, -0.6999999986344048741 ) ) ;
#5347=CARTESIAN_POINT ( 'NONE',  ( -1.301042606982605321E-15, 7.505553499465137612, -0.5805565836007695601 ) ) ;
#5388=CARTESIAN_POINT ( 'NONE',  ( 3.458734125000000770, -1.432654583217639610, -2.824999998634404985 ) ) ;
#5390=ORIENTED_EDGE ( 'NONE', *, *, #2492, .T. ) ;
#5407=CARTESIAN_POINT ( 'NONE',  ( 4.000000000000000888, -1.656854249492379694, 4.737499999999999822 ) ) ;
#5417=CARTESIAN_POINT ( 'NONE',  ( -2.449293598294706907E-16, 4.000000000000000000, 1.175000002731187543 ) ) ;
#5434=CARTESIAN_POINT ( 'NONE',  ( -2.740672138314428796, -2.121953112084053128, 2.039999999999995595 ) ) ;
#5442=CARTESIAN_POINT ( 'NONE',  ( -1.432654583217640276, 3.458734125000000326, 5.550000001365596347 ) ) ;
#5445=ORIENTED_EDGE ( 'NONE', *, *, #17425, .T. ) ;
#5453=CARTESIAN_POINT ( 'NONE',  ( 1.432654583217642053, -3.458734124999999882, 1.300000001365597013 ) ) ;
#5460=CARTESIAN_POINT ( 'NONE',  ( 6.353591512924457348E-16, -3.458734125000000326, 0.9875000013655956810 ) ) ;
#5465=CARTESIAN_POINT ( 'NONE',  ( 6.500000000000000888, 0.000000000000000000, -3.700000000000000178 ) ) ;
#5487=CARTESIAN_POINT ( 'NONE',  ( 3.194497824546384646, 2.392783823000994570, 2.039999999999998259 ) ) ;
#5501=CARTESIAN_POINT ( 'NONE',  ( -3.458734125000000326, 1.432654583217640276, -1.324999998634403653 ) ) ;
#5502=DIRECTION ( 'NONE',  ( -0.000000000000000000, -0.000000000000000000, 1.000000000000000000 ) ) ;
#5517=CARTESIAN_POINT ( 'NONE',  ( -1.432654583217640498, 3.458734125000000770, -3.199999998634403209 ) ) ;
#5556=CARTESIAN_POINT ( 'NONE',  ( -2.828427124746189403, -2.828427124746190735, -2.449999997268812457 ) ) ;
#5559=CARTESIAN_POINT ( 'NONE',  ( -3.250000000000003997, -5.629165124598848102, 1.734723475976807094E-15 ) ) ;
#5560=ORIENTED_EDGE ( 'NONE', *, *, #14173, .T. ) ;
#5562=CARTESIAN_POINT ( 'NONE',  ( -4.000000000000000000, -1.656854249492383024, -2.637499999999998845 ) ) ;
#5563=CARTESIAN_POINT ( 'NONE',  ( 1.656854249492380138, 4.000000000000000000, -2.887499997268812457 ) ) ;
#5565=EDGE_CURVE ( 'NONE', #15405, #844, #11058, .T. ) ;
#5569=CARTESIAN_POINT ( 'NONE',  ( 3.458734125000000770, 1.432654583217640498, -0.4499999986344046521 ) ) ;
#5576=CARTESIAN_POINT ( 'NONE',  ( 6.353591512924457348E-16, -3.458734125000000326, 1.987500001365596569 ) ) ;
#5596=ADVANCED_FACE ( 'NONE', ( #2813 ), #22066, .F. ) ;
#5602=CARTESIAN_POINT ( 'NONE',  ( -4.623144047065556705, -4.836380039389426955, -3.593844378834464059 ) ) ;
#5607=CARTESIAN_POINT ( 'NONE',  ( 1.065083781909167193, -6.890627091270381754, -3.442152416367922463 ) ) ;
#5621=CARTESIAN_POINT ( 'NONE',  ( -4.000000000000000000, 0.000000000000000000, 1.300000000000000711 ) ) ;
#5631=ORIENTED_EDGE ( 'NONE', *, *, #21627, .F. ) ;
#5634=CARTESIAN_POINT ( 'NONE',  ( 6.499999999999999112, 0.000000000000000000, 1.734723475976807094E-15 ) ) ;
#5638=CARTESIAN_POINT ( 'NONE',  ( 3.458734125000000770, 1.432654583217640498, -2.449999998634404097 ) ) ;
#5639=CARTESIAN_POINT ( 'NONE',  ( 4.000000000000000000, 4.898587196589412829E-16, -3.074999997268812901 ) ) ;
#5674=CARTESIAN_POINT ( 'NONE',  ( 1.432654583217639832, 3.458734125000000326, 5.425000001365595459 ) ) ;
#5679=CARTESIAN_POINT ( 'NONE',  ( -2.228340424525890907E-16, 3.639156083333333846, -3.158333332422934348 ) ) ;
#5680=CARTESIAN_POINT ( 'NONE',  ( 4.000000000000000000, 1.656854249492381248, -3.012499997268812901 ) ) ;
#5684=AXIS2_PLACEMENT_3D ( 'NONE', #14006, #4765, #15916 ) ;
#5685=CARTESIAN_POINT ( 'NONE',  ( -2.445694354108819635, -2.445694354108820967, 1.112500001365595681 ) ) ;
#5694=CARTESIAN_POINT ( 'NONE',  ( 1.432654583217642275, -3.458734124999999437, 1.050000001365596791 ) ) ;
#5728=CARTESIAN_POINT ( 'NONE',  ( 3.799967015292484707, 0.6806254479988701478, 2.040000000000004476 ) ) ;
#5735=CARTESIAN_POINT ( 'NONE',  ( -2.974182810908594821, 5.788408252967899514, 4.456522679820626832E-15 ) ) ;
#5742=FACE_OUTER_BOUND ( 'NONE', #3475, .T. ) ;
#5748=ORIENTED_EDGE ( 'NONE', *, *, #20299, .F. ) ;
#5766=CARTESIAN_POINT ( 'NONE',  ( -1.432654583217641164, -3.458734125000000326, -0.8249999986344030978 ) ) ;
#5767=CARTESIAN_POINT ( 'NONE',  ( -2.117863837641485618E-16, 3.458734125000000770, -3.262499998634402765 ) ) ;
#5771=ORIENTED_EDGE ( 'NONE', *, *, #20199, .F. ) ;
#5790=CARTESIAN_POINT ( 'NONE',  ( -2.445694354108820523, 2.445694354108820523, 5.862500001365596347 ) ) ;
#5797=ORIENTED_EDGE ( 'NONE', *, *, #13190, .F. ) ;
#5799=CARTESIAN_POINT ( 'NONE',  ( -1.432654583217640942, -3.458734124999999882, 3.925000001365594127 ) ) ;
#5802=ORIENTED_EDGE ( 'NONE', *, *, #15414, .F. ) ;
#5809=CARTESIAN_POINT ( 'NONE',  ( -3.458734125000000770, 0.000000000000000000, -0.01249999863440348635 ) ) ;
#5814=CARTESIAN_POINT ( 'NONE',  ( -3.458734125000000326, 1.432654583217640276, 0.6750000013655963471 ) ) ;
#5840=CARTESIAN_POINT ( 'NONE',  ( 2.828427124746189847, 2.828427124746190291, 0.05000000273118650196 ) ) ;
#5842=CARTESIAN_POINT ( 'NONE',  ( 3.250000000000002665, -5.629165124598850767, -3.700000000000000178 ) ) ;
#5846=CARTESIAN_POINT ( 'NONE',  ( -2.149058192116894084, 6.264794173742276762, -0.06682554136337909290 ) ) ;
#5857=CONICAL_SURFACE ( 'NONE', #19234, 6.500000000000000888, 1.047197551196596521 ) ;
#5859=CARTESIAN_POINT ( 'NONE',  ( -2.828427124746190291, 2.828427124746190291, -2.824999999999997513 ) ) ;
#5881=CARTESIAN_POINT ( 'NONE',  ( 1.656854249492380360, 4.000000000000000000, 0.9875000000000008216 ) ) ;
#5893=ORIENTED_EDGE ( 'NONE', *, *, #3532, .F. ) ;
#5901=EDGE_CURVE ( 'NONE', #438, #21232, #9150, .T. ) ;
#5908=CARTESIAN_POINT ( 'NONE',  ( 2.445694354108820967, -2.445694354108820079, 4.362500001365595459 ) ) ;
#5916=CARTESIAN_POINT ( 'NONE',  ( -3.458734125000000326, 1.432654583217640276, 1.675000001365597235 ) ) ;
#5921=CARTESIAN_POINT ( 'NONE',  ( -2.828427124746189403, -2.828427124746190735, -2.574999999999999289 ) ) ;
#5922=AXIS2_PLACEMENT_3D ( 'NONE', #15042, #20026, #20384 ) ;
#5928=CARTESIAN_POINT ( 'NONE',  ( -2.117863837641485618E-16, 3.458734125000000770, 1.737500001365596347 ) ) ;
#5936=CARTESIAN_POINT ( 'NONE',  ( 3.458734125000000770, 4.235727675282972223E-16, 4.487500001365595459 ) ) ;
#5951=CARTESIAN_POINT ( 'NONE',  ( 0.000000000000000000, 0.000000000000000000, 19.04999999999996874 ) ) ;
#5954=VECTOR ( 'NONE', #15610, 1000.000000000000000 ) ;
#5974=ORIENTED_EDGE ( 'NONE', *, *, #2562, .F. ) ;
#5981=CARTESIAN_POINT ( 'NONE',  ( -4.000000000000000000, 0.000000000000000000, 1.300000000000000711 ) ) ;
#5996=CARTESIAN_POINT ( 'NONE',  ( -3.458734125000000326, -1.432654583217642497, -0.9499999986344030978 ) ) ;
#5997=CARTESIAN_POINT ( 'NONE',  ( 2.828427124746189847, 2.828427124746190291, 2.925000000000002043 ) ) ;
#6005=ORIENTED_EDGE ( 'NONE', *, *, #1743, .F. ) ;
#6009=SHAPE_DEFINITION_REPRESENTATION ( #14894, #1939 ) ;
#6025=CARTESIAN_POINT ( 'NONE',  ( 3.458734125000000770, 1.432654583217640498, 4.550000001365596347 ) ) ;
#6030=VECTOR ( 'NONE', #18057, 1000.000000000000000 ) ;
#6036=CARTESIAN_POINT ( 'NONE',  ( -1.432654583217640276, 3.458734125000000326, 1.550000001365597013 ) ) ;
#6038=ORIENTED_EDGE ( 'NONE', *, *, #671, .T. ) ;
#6042=VERTEX_POINT ( 'NONE', #3553 ) ;
#6045=CARTESIAN_POINT ( 'NONE',  ( 3.458734125000001214, -1.432654583217639610, -2.574999998634404541 ) ) ;
#6053=CARTESIAN_POINT ( 'NONE',  ( -3.458734125000000326, -1.432654583217642497, 4.050000001365596347 ) ) ;
#6061=CARTESIAN_POINT ( 'NONE',  ( -4.000000000000000000, 0.000000000000000000, 2.425000002731188431 ) ) ;
#6069=FACE_OUTER_BOUND ( 'NONE', #17881, .T. ) ;
#6073=CARTESIAN_POINT ( 'NONE',  ( 4.000000000000000000, 4.898587196589412829E-16, -2.074999997268812013 ) ) ;
#6083=CARTESIAN_POINT ( 'NONE',  ( 4.000000000000000888, -1.656854249492379694, 0.7375000000000022649 ) ) ;
#6086=ORIENTED_EDGE ( 'NONE', *, *, #6871, .T. ) ;
#6120=CARTESIAN_POINT ( 'NONE',  ( 4.000000000000000000, 1.656854249492381248, -0.1374999999999984013 ) ) ;
#6123=B_SPLINE_CURVE_WITH_KNOTS ( 'NONE', 3,
 ( #21645, #23580, #12598, #20317, #19970, #14736 ),
 .UNSPECIFIED., .F., .F.,
 ( 4, 2, 4 ),
 ( 2.380733003329261875E-07, 0.001898835937927393497, 0.003797433802554454115 ),
 .UNSPECIFIED. ) ;
#6124=CARTESIAN_POINT ( 'NONE',  ( 2.828427124746189847, 2.828427124746190291, -1.074999999999997735 ) ) ;
#6131=B_SPLINE_CURVE_WITH_KNOTS ( 'NONE', 3,
 ( #8749, #21530, #6823, #21412, #6953, #2748, #22867, #6481, #13803, #8999, #3465, #16806, #12827, #19740, #12601, #21772 ),
 .UNSPECIFIED., .F., .F.,
 ( 4, 2, 2, 2, 2, 2, 2, 4 ),
 ( 0.000000000000000000, 0.001180799220441102609, 0.001771198830661654131, 0.002361598440882205219, 0.002951998051102756523, 0.003542397661323308262, 0.004132797271543859133, 0.004723196881764409570 ),
 .UNSPECIFIED. ) ;
#6151=CARTESIAN_POINT ( 'NONE',  ( 6.353591512924457348E-16, -3.458734125000000770, 3.237500001365597679 ) ) ;
#6157=CYLINDRICAL_SURFACE ( 'NONE', #3227, 4.000000000000000000 ) ;
#6161=CARTESIAN_POINT ( 'NONE',  ( 3.458734125000000326, 4.235727675282971730E-16, 3.237500001365597679 ) ) ;
#6163=CARTESIAN_POINT ( 'NONE',  ( 1.432654583217639832, 3.458734125000000326, 0.4250000013655961251 ) ) ;
#6166=FILL_AREA_STYLE ('',( #11936 ) ) ;
#6181=CARTESIAN_POINT ( 'NONE',  ( 1.432654583217642275, -3.458734124999999437, -2.949999998634404985 ) ) ;
#6188=CARTESIAN_POINT ( 'NONE',  ( 1.656854249492380360, 4.000000000000000000, 3.112500002731188875 ) ) ;
#6211=CARTESIAN_POINT ( 'NONE',  ( -4.000000000000000000, 0.000000000000000000, -3.574999997268813345 ) ) ;
#6220=CARTESIAN_POINT ( 'NONE',  ( 0.5316568767328664347, 7.198601258566900363, -0.4033376246892524941 ) ) ;
#6226=CARTESIAN_POINT ( 'NONE',  ( 1.067197363239223984, 6.889406814520512512, -3.442664554191215753 ) ) ;
#6227=DIRECTION ( 'NONE',  ( 0.000000000000000000, 0.000000000000000000, -1.000000000000000000 ) ) ;
#6230=CARTESIAN_POINT ( 'NONE',  ( 4.000000000000000000, 4.898587196589412829E-16, 0.9250000027311873207 ) ) ;
#6235=ADVANCED_FACE ( 'NONE', ( #3782 ), #10642, .T. ) ;
#6238=CARTESIAN_POINT ( 'NONE',  ( -2.449293598294706907E-16, 4.000000000000000000, 0.05000000000000143219 ) ) ;
#6243=EDGE_LOOP ( 'NONE', ( #11239, #16584, #4919, #18935 ) ) ;
#6249=LINE ( 'NONE', #22759, #5954 ) ;
#6264=CLOSED_SHELL ( 'NONE', ( #7600, #1733, #21363, #9358, #19344, #17870, #14789, #19776, #14472, #21696, #15928, #10706, #16813, #7027, #14271, #20031, #9165, #708, #10005, #11588, #20368, #18739, #17383, #752, #9003, #18263, #142, #6235, #2204, #6997, #13643, #2277, #9274, #9664, #8621, #22119, #19165, #22942, #11576, #10376, #612, #11297, #5596, #19605 ) ) ;
#6265=CARTESIAN_POINT ( 'NONE',  ( -3.458734125000000326, -1.432654583217642497, 3.050000001365598568 ) ) ;
#6276=CARTESIAN_POINT ( 'NONE',  ( 2.445694354108820079, 2.445694354108820523, 0.3625000013655951259 ) ) ;
#6278=CARTESIAN_POINT ( 'NONE',  ( -2.445694354108819635, -2.445694354108820523, 1.862500001365596347 ) ) ;
#6286=CARTESIAN_POINT ( 'NONE',  ( -3.458734125000000770, 1.432654583217640498, -2.074999998634404097 ) ) ;
#6297=CARTESIAN_POINT ( 'NONE',  ( -2.117863837641485618E-16, 3.458734125000000326, -3.512499998634403209 ) ) ;
#6302=CARTESIAN_POINT ( 'NONE',  ( 8.673617379884035472E-16, 7.505553499465136724, -3.700000000000000178 ) ) ;
#6307=CARTESIAN_POINT ( 'NONE',  ( -4.000000000000000888, 1.656854249492380804, 5.362500002731188431 ) ) ;
#6318=AXIS2_PLACEMENT_3D ( 'NONE', #5327, #3409, #12779 ) ;
#6338=CARTESIAN_POINT ( 'NONE',  ( -4.000000000000000000, 0.000000000000000000, -0.5749999972688123462 ) ) ;
#6346=CARTESIAN_POINT ( 'NONE',  ( -1.647987302177966740E-14, -7.505553499465137612, -3.119443416399232394 ) ) ;
#6361=CARTESIAN_POINT ( 'NONE',  ( -4.000000000000000888, 1.656854249492380804, 3.237500000000002931 ) ) ;
#6363=CARTESIAN_POINT ( 'NONE',  ( 4.000000000000000000, 4.898587196589412829E-16, -0.07499999726881187434 ) ) ;
#6364=CARTESIAN_POINT ( 'NONE',  ( -4.000000000000000000, 0.000000000000000000, -0.6999999999999975131 ) ) ;
#6368=ORIENTED_EDGE ( 'NONE', *, *, #15144, .T. ) ;
#6370=( BOUNDED_CURVE ( )  B_SPLINE_CURVE ( 2, ( #2291, #3722, #376, #20486, #5417, #20007, #22279, #4087, #14782 ),
 .UNSPECIFIED., .F., .F. ) 
 B_SPLINE_CURVE_WITH_KNOTS ( ( 3, 2, 2, 2, 3 ),
 ( 0.4000000000000000222, 0.4124999999999999778, 0.4249999999999999889, 0.4375000000000000000, 0.4500000000000000111 ),
 .UNSPECIFIED. ) 
 CURVE ( )  GEOMETRIC_REPRESENTATION_ITEM ( )  RATIONAL_B_SPLINE_CURVE ( ( 1.000000000000000000, 0.9238795325112867385, 1.000000000000000000, 0.9238795325112867385, 1.000000000000000000, 0.9238795325112867385, 1.000000000000000000, 0.9238795325112867385, 1.000000000000000000 ) ) 
 REPRESENTATION_ITEM ( '' )  );
#6383=CARTESIAN_POINT ( 'NONE',  ( 1.432654583217640276, 3.458734125000000770, 4.675000001365594571 ) ) ;
#6386=FACE_BOUND ( 'NONE', #15366, .T. ) ;
#6391=CARTESIAN_POINT ( 'NONE',  ( -1.432654583217640942, -3.458734124999999882, 1.925000001365597457 ) ) ;
#6392=CARTESIAN_POINT ( 'NONE',  ( -3.458734125000000326, 0.000000000000000000, -1.262499998634402765 ) ) ;
#6397=VERTEX_POINT ( 'NONE', #6553 ) ;
#6417=CARTESIAN_POINT ( 'NONE',  ( -2.117863837641485618E-16, 3.458734125000000770, 0.7375000013655954589 ) ) ;
#6424=CARTESIAN_POINT ( 'NONE',  ( 2.828427124746190735, -2.828427124746189847, 2.800000002731188875 ) ) ;
#6433=EDGE_CURVE ( 'NONE', #7689, #13210, #10656, .T. ) ;
#6460=CARTESIAN_POINT ( 'NONE',  ( 4.350941807883110357, 4.993536075455422996, -3.633174458636621917 ) ) ;
#6467=CIRCLE ( 'NONE', #9920, 4.714285714285714413 ) ;
#6481=CARTESIAN_POINT ( 'NONE',  ( -2.021686707278909978, 2.813123132921495628, -3.295601554149325541 ) ) ;
#6484=CARTESIAN_POINT ( 'NONE',  ( -4.000000000000000888, 1.656854249492380582, -0.7624999999999970690 ) ) ;
#6486=ORIENTED_EDGE ( 'NONE', *, *, #9854, .T. ) ;
#6493=ORIENTED_EDGE ( 'NONE', *, *, #2441, .T. ) ;
#6502=EDGE_CURVE ( 'NONE', #15405, #10489, #20120, .T. ) ;
#6509=CARTESIAN_POINT ( 'NONE',  ( 1.432654583217640276, 3.458734125000000770, 1.675000001365597235 ) ) ;
#6519=CARTESIAN_POINT ( 'NONE',  ( -3.458734125000000326, 1.432654583217640276, 0.6750000013655963471 ) ) ;
#6520=ORIENTED_EDGE ( 'NONE', *, *, #13815, .F. ) ;
#6529=CARTESIAN_POINT ( 'NONE',  ( -3.458734125000000770, 0.000000000000000000, -3.012499998634404541 ) ) ;
#6531=CARTESIAN_POINT ( 'NONE',  ( 0.000000000000000000, 0.000000000000000000, -3.674599999999999866 ) ) ;
#6540=CARTESIAN_POINT ( 'NONE',  ( -2.445694354108820523, 2.445694354108820523, -0.1374999986344035974 ) ) ;
#6550=CARTESIAN_POINT ( 'NONE',  ( -1.656854249492380804, 4.000000000000000000, 2.237500002731187987 ) ) ;
#6553=CARTESIAN_POINT ( 'NONE',  ( -3.250000000000004885, -5.629165124598848990, -3.700000000000000178 ) ) ;
#6557=TOROIDAL_SURFACE ( 'NONE', #8103, 5.479999999999998650, 1.020000000000000018 ) ;
#6562=CARTESIAN_POINT ( 'NONE',  ( 0.000000000000000000, 0.000000000000000000, 2.040000000000001812 ) ) ;
#6564=CARTESIAN_POINT ( 'NONE',  ( -2.445694354108819635, -2.445694354108820523, 2.862500001365597235 ) ) ;
#6596=CARTESIAN_POINT ( 'NONE',  ( -4.000000000000000000, 0.000000000000000000, -1.699999999999998401 ) ) ;
#6603=EDGE_LOOP ( 'NONE', ( #20716, #21468, #4243, #22139 ) ) ;
#6606=EDGE_CURVE ( 'NONE', #3610, #4306, #1490, .T. ) ;
#6620=CARTESIAN_POINT ( 'NONE',  ( -2.445694354108820523, 2.445694354108820523, -0.1374999986344035974 ) ) ;
#6621=DIRECTION ( 'NONE',  ( -0.000000000000000000, -0.000000000000000000, 1.000000000000000000 ) ) ;
#6631=EDGE_CURVE ( 'NONE', #20551, #15816, #22373, .T. ) ;
#6633=CARTESIAN_POINT ( 'NONE',  ( 6.353591512924457348E-16, -3.458734125000000326, 1.987500001365596569 ) ) ;
#6654=CARTESIAN_POINT ( 'NONE',  ( -3.458734125000000326, -1.432654583217642497, 2.050000001365597679 ) ) ;
#6660=DIRECTION ( 'NONE',  ( -1.000000000000000000, 0.000000000000000000, 0.000000000000000000 ) ) ;
#6664=CARTESIAN_POINT ( 'NONE',  ( -1.656854249492380804, 4.000000000000000000, 1.237500002731187099 ) ) ;
#6677=FACE_OUTER_BOUND ( 'NONE', #13709, .T. ) ;
#6679=CYLINDRICAL_SURFACE ( 'NONE', #13613, 4.000000000000000000 ) ;
#6682=CARTESIAN_POINT ( 'NONE',  ( -3.561348994077910834, 0.3690845827472539198, 2.039999999999996927 ) ) ;
#6684=ORIENTED_EDGE ( 'NONE', *, *, #20323, .T. ) ;
#6695=EDGE_CURVE ( 'NONE', #23104, #11298, #12333, .T. ) ;
#6701=CARTESIAN_POINT ( 'NONE',  ( 1.656854249492383024, -3.999999999999999112, -1.262499997268811125 ) ) ;
#6712=CARTESIAN_POINT ( 'NONE',  ( 7.347880794884118750E-16, -4.000000000000000000, 0.6750000027311870987 ) ) ;
#6737=CARTESIAN_POINT ( 'NONE',  ( 3.458734125000000770, 4.235727675282972223E-16, 0.4875000013655969577 ) ) ;
#6765=CARTESIAN_POINT ( 'NONE',  ( -2.445694354108819635, -2.445694354108820967, 2.112500001365596791 ) ) ;
#6774=CARTESIAN_POINT ( 'NONE',  ( -1.656854249492381248, -3.999999999999999112, -1.387499997268811125 ) ) ;
#6788=B_SPLINE_CURVE_WITH_KNOTS ( 'NONE', 3,
 ( #12345, #15704, #8387, #933, #4772, #12108 ),
 .UNSPECIFIED., .F., .F.,
 ( 4, 2, 4 ),
 ( 2.380733003139562494E-07, 0.001898835937927376150, 0.003797433802554438069 ),
 .UNSPECIFIED. ) ;
#6791=CARTESIAN_POINT ( 'NONE',  ( 2.445694354108820079, 2.445694354108820523, 2.362500001365596791 ) ) ;
#6794=CONICAL_SURFACE ( 'NONE', #23223, 6.500000000000000888, 1.047197551196596521 ) ;
#6797=CARTESIAN_POINT ( 'NONE',  ( -2.154698047631601110, 3.153627145295581524, 2.039999999999997371 ) ) ;
#6821=CARTESIAN_POINT ( 'NONE',  ( -6.499999999999999112, -1.264206540070614615, -3.645490429492275197 ) ) ;
#6823=CARTESIAN_POINT ( 'NONE',  ( -3.149734950108402654, 1.481481450868026295, -3.295601554149321988 ) ) ;
#6830=CARTESIAN_POINT ( 'NONE',  ( 3.458734125000000326, 4.235727675282971730E-16, -0.7624999986344040970 ) ) ;
#6844=VECTOR ( 'NONE', #19554, 1000.000000000000000 ) ;
#6849=CARTESIAN_POINT ( 'NONE',  ( -3.458734125000000770, 0.000000000000000000, -2.012499998634403653 ) ) ;
#6853=CARTESIAN_POINT ( 'NONE',  ( 4.000000000000000000, 4.898587196589412829E-16, -2.199999999999998845 ) ) ;
#6864=CARTESIAN_POINT ( 'NONE',  ( 3.458734125000001214, -1.432654583217639610, -1.824999998634404097 ) ) ;
#6868=ORIENTED_EDGE ( 'NONE', *, *, #15214, .F. ) ;
#6871=EDGE_CURVE ( 'NONE', #5142, #21452, #14100, .T. ) ;
#6879=CARTESIAN_POINT ( 'NONE',  ( -4.000000000000000000, -1.656854249492383024, -2.512499997268812457 ) ) ;
#6880=AXIS2_PLACEMENT_3D ( 'NONE', #12463, #14612, #3324 ) ;
#6886=CARTESIAN_POINT ( 'NONE',  ( 2.445694354108820079, 2.445694354108820523, 1.612500001365596125 ) ) ;
#6896=CARTESIAN_POINT ( 'NONE',  ( -1.656854249492380804, 4.000000000000000000, -0.7624999972688126793 ) ) ;
#6901=CARTESIAN_POINT ( 'NONE',  ( 3.250000000000001776, -5.629165124598848990, 1.734723475976807094E-15 ) ) ;
#6915=MANIFOLD_SOLID_BREP ( 'Cavity1', #6264 ) ;
#6916=LINE ( 'NONE', #61, #19119 ) ;
#6918=CARTESIAN_POINT ( 'NONE',  ( 3.458734125000000326, 4.235727675282971730E-16, 3.237500001365597679 ) ) ;
#6924=CARTESIAN_POINT ( 'NONE',  ( -0.3508590460142260725, 3.955718283038086369, 2.039999999999998259 ) ) ;
#6946=DIRECTION ( 'NONE',  ( 0.000000000000000000, -0.000000000000000000, 1.000000000000000000 ) ) ;
#6953=CARTESIAN_POINT ( 'NONE',  ( -2.724039609044899724, 2.140243184150454780, -3.295601554149323320 ) ) ;
#6958=CARTESIAN_POINT ( 'NONE',  ( 6.353591512924457348E-16, -3.458734125000000326, -2.012499998634403653 ) ) ;
#6967=FACE_OUTER_BOUND ( 'NONE', #23028, .T. ) ;
#6973=CARTESIAN_POINT ( 'NONE',  ( -1.432654583217640498, 3.458734125000000770, 0.8000000013655964581 ) ) ;
#6984=CARTESIAN_POINT ( 'NONE',  ( -3.458734124999999882, -1.432654583217642275, -2.199999998634404097 ) ) ;
#6987=EDGE_LOOP ( 'NONE', ( #3555, #13979, #20675, #14722 ) ) ;
#6989=VERTEX_POINT ( 'NONE', #4823 ) ;
#6992=( BOUNDED_CURVE ( )  B_SPLINE_CURVE ( 2, ( #18269, #8968, #21967, #14710, #1510, #17926, #16370, #14239, #66 ),
 .UNSPECIFIED., .F., .F. ) 
 B_SPLINE_CURVE_WITH_KNOTS ( ( 3, 2, 2, 2, 3 ),
 ( 0.5999999999999999778, 0.6125000000000000444, 0.6250000000000000000, 0.6374999999999999556, 0.6500000000000000222 ),
 .UNSPECIFIED. ) 
 CURVE ( )  GEOMETRIC_REPRESENTATION_ITEM ( )  RATIONAL_B_SPLINE_CURVE ( ( 1.000000000000000000, 0.9238795325112867385, 1.000000000000000000, 0.9238795325112867385, 1.000000000000000000, 0.9238795325112867385, 1.000000000000000000, 0.9238795325112867385, 1.000000000000000000 ) ) 
 REPRESENTATION_ITEM ( '' )  );
#6997=ADVANCED_FACE ( 'NONE', ( #23027 ), #9516, .T. ) ;
#7002=CARTESIAN_POINT ( 'NONE',  ( -2.117863837641485618E-16, 3.458734125000000770, -3.262499998634402765 ) ) ;
#7010=VERTEX_POINT ( 'NONE', #1102 ) ;
#7012=CARTESIAN_POINT ( 'NONE',  ( -2.449293598294706907E-16, 4.000000000000000000, -0.8249999972688125682 ) ) ;
#7022=CARTESIAN_POINT ( 'NONE',  ( 0.000000000000000000, 0.000000000000000000, -3.674599999999999866 ) ) ;
#7027=ADVANCED_FACE ( 'NONE', ( #2675 ), #17420, .F. ) ;
#7034=CARTESIAN_POINT ( 'NONE',  ( -3.458734124999999882, -1.432654583217642497, 3.800000001365595459 ) ) ;
#7035=EDGE_CURVE ( 'NONE', #16269, #18845, #12197, .T. ) ;
#7053=VECTOR ( 'NONE', #15900, 1000.000000000000000 ) ;
#7075=CARTESIAN_POINT ( 'NONE',  ( -1.432654583217640942, -3.458734124999999882, -2.074999998634404097 ) ) ;
#7079=VERTEX_POINT ( 'NONE', #22907 ) ;
#7096=CARTESIAN_POINT ( 'NONE',  ( -2.449293598294706907E-16, 4.000000000000000000, 4.049999999999999822 ) ) ;
#7107=CARTESIAN_POINT ( 'NONE',  ( 6.353591512924457348E-16, -3.458734125000000326, -2.012499998634403653 ) ) ;
#7126=CARTESIAN_POINT ( 'NONE',  ( 2.445694354108820079, 2.445694354108820523, -2.387499998634403653 ) ) ;
#7127=CARTESIAN_POINT ( 'NONE',  ( -1.313672045791830501, -3.207643946584868289, 2.039999999999997815 ) ) ;
#7134=CARTESIAN_POINT ( 'NONE',  ( -1.656854249492381248, -3.999999999999999112, 0.6125000027311866546 ) ) ;
#7136=ORIENTED_EDGE ( 'NONE', *, *, #11264, .T. ) ;
#7147=EDGE_CURVE ( 'NONE', #11298, #20551, #3420, .T. ) ;
#7153=CARTESIAN_POINT ( 'NONE',  ( -3.458734124999999882, -1.432654583217642497, 0.8000000013655964581 ) ) ;
#7160=CARTESIAN_POINT ( 'NONE',  ( -6.500000000000001776, 0.6345343291280540754, -3.700000000000001066 ) ) ;
#7161=DIRECTION ( 'NONE',  ( -0.000000000000000000, -0.000000000000000000, 1.000000000000000000 ) ) ;
#7184=CARTESIAN_POINT ( 'NONE',  ( -6.500000000000000000, 0.000000000000000000, 1.734723475976807094E-15 ) ) ;
#7186=CARTESIAN_POINT ( 'NONE',  ( 2.813044857425830880, -2.271656904766521823, 2.040000000000001368 ) ) ;
#7193=DIRECTION ( 'NONE',  ( 0.000000000000000000, 0.000000000000000000, 1.000000000000000000 ) ) ;
#7200=CARTESIAN_POINT ( 'NONE',  ( -2.117863837641485618E-16, 3.458734125000000326, -0.5124999986344038749 ) ) ;
#7213=AXIS2_PLACEMENT_3D ( 'NONE', #13368, #13716, #13488 ) ;
#7222=CARTESIAN_POINT ( 'NONE',  ( -2.828427124746189403, -2.828427124746190735, 5.425000000000000711 ) ) ;
#7249=CARTESIAN_POINT ( 'NONE',  ( 0.000000000000000000, 0.000000000000000000, 0.000000000000000000 ) ) ;
#7259=CARTESIAN_POINT ( 'NONE',  ( 4.000000000000000000, 4.898587196589412829E-16, -2.074999997268812013 ) ) ;
#7261=ORIENTED_EDGE ( 'NONE', *, *, #17014, .T. ) ;
#7272=CARTESIAN_POINT ( 'NONE',  ( 1.432654583217640276, 3.458734125000000770, 1.675000001365597235 ) ) ;
#7281=CARTESIAN_POINT ( 'NONE',  ( -2.117863837641485618E-16, 3.458734125000000326, -1.512499998634402987 ) ) ;
#7318=AXIS2_PLACEMENT_3D ( 'NONE', #3111, #10686, #17843 ) ;
#7342=CARTESIAN_POINT ( 'NONE',  ( -1.656854249492381248, -3.999999999999999112, -0.3874999972688122907 ) ) ;
#7345=CARTESIAN_POINT ( 'NONE',  ( 7.347880794884118750E-16, -4.000000000000000000, 3.550000000000002931 ) ) ;
#7381=CARTESIAN_POINT ( 'NONE',  ( -3.458734125000000326, 1.432654583217640276, 5.675000001365596347 ) ) ;
#7387=VERTEX_POINT ( 'NONE', #20916 ) ;
#7390=CARTESIAN_POINT ( 'NONE',  ( -3.458734125000000326, -1.432654583217642497, -0.9499999986344030978 ) ) ;
#7395=CARTESIAN_POINT ( 'NONE',  ( -3.458734125000000326, 1.432654583217640276, -0.3249999986344045411 ) ) ;
#7424=CARTESIAN_POINT ( 'NONE',  ( 2.974182810908596597, -5.788408252967910173, -3.700000000000000178 ) ) ;
#7430=DIRECTION ( 'NONE',  ( -1.000000000000000000, 0.000000000000000000, 0.000000000000000000 ) ) ;
#7436=EDGE_LOOP ( 'NONE', ( #13337, #14281, #4682, #12013 ) ) ;
#7438=ORIENTED_EDGE ( 'NONE', *, *, #3345, .F. ) ;
#7454=CARTESIAN_POINT ( 'NONE',  ( 2.828427124746190735, -2.828427124746189847, 5.675000000000001599 ) ) ;
#7490=( NAMED_UNIT ( * ) PLANE_ANGLE_UNIT ( ) SI_UNIT ( $, .RADIAN. ) );
#7491=CARTESIAN_POINT ( 'NONE',  ( -2.828427124746189403, -2.828427124746190735, -3.449999997268813345 ) ) ;
#7496=CARTESIAN_POINT ( 'NONE',  ( 1.656854249492383024, -3.999999999999999112, -2.387499999999998401 ) ) ;
#7502=CARTESIAN_POINT ( 'NONE',  ( -1.432654583217641164, -3.458734125000000326, 1.175000001365597013 ) ) ;
#7510=CARTESIAN_POINT ( 'NONE',  ( 3.458734125000000326, 4.235727675282971730E-16, -0.7624999986344040970 ) ) ;
#7525=VERTEX_POINT ( 'NONE', #19720 ) ;
#7527=EDGE_CURVE ( 'NONE', #8578, #10489, #12100, .T. ) ;
#7555=CARTESIAN_POINT ( 'NONE',  ( -4.350525068611870161, 4.993776679985856504, -3.644669744206380013 ) ) ;
#7565=CARTESIAN_POINT ( 'NONE',  ( 1.656854249492383024, -3.999999999999999112, -0.2624999972688121797 ) ) ;
#7568=DIRECTION ( 'NONE',  ( -0.000000000000000000, -0.000000000000000000, 1.000000000000000000 ) ) ;
#7570=CARTESIAN_POINT ( 'NONE',  ( -3.458734125000000326, -1.432654583217642497, -1.949999998634404319 ) ) ;
#7571=CARTESIAN_POINT ( 'NONE',  ( 4.000000000000000000, 1.656854249492381248, 4.862500000000001599 ) ) ;
#7586=EDGE_LOOP ( 'NONE', ( #4546, #4744, #19169, #17631 ) ) ;
#7599=CARTESIAN_POINT ( 'NONE',  ( -3.458734125000000770, 0.000000000000000000, 5.987500001365596347 ) ) ;
#7600=ADVANCED_FACE ( 'NONE', ( #22816 ), #2458, .T. ) ;
#7609=CARTESIAN_POINT ( 'NONE',  ( 2.445694354108820523, -2.445694354108820079, 4.112500001365594571 ) ) ;
#7629=CARTESIAN_POINT ( 'NONE',  ( -2.445694354108819635, -2.445694354108820523, 1.862500001365596347 ) ) ;
#7654=ORIENTED_EDGE ( 'NONE', *, *, #20761, .F. ) ;
#7658=CARTESIAN_POINT ( 'NONE',  ( 3.280735753986837366, -1.667205581200902120, 2.040000000000033786 ) ) ;
#7664=CARTESIAN_POINT ( 'NONE',  ( 4.350525068611871049, -4.993776679985862721, -3.644669744206375572 ) ) ;
#7683=CYLINDRICAL_SURFACE ( 'NONE', #1460, 4.000000000000000000 ) ;
#7689=VERTEX_POINT ( 'NONE', #22455 ) ;
#7698=CARTESIAN_POINT ( 'NONE',  ( -2.828427124746189403, -2.828427124746190735, 1.425000000000000933 ) ) ;
#7704=ORIENTED_EDGE ( 'NONE', *, *, #9384, .F. ) ;
#7718=B_SPLINE_CURVE_WITH_KNOTS ( 'NONE', 3,
 ( #12825, #16752, #9587, #7664, #9342, #16879 ),
 .UNSPECIFIED., .F., .F.,
 ( 4, 2, 4 ),
 ( 2.380733003149452133E-07, 0.001898835937927375499, 0.003797433802554436334 ),
 .UNSPECIFIED. ) ;
#7733=CARTESIAN_POINT ( 'NONE',  ( 4.000000000000000888, -1.656854249492379694, -3.137499997268812901 ) ) ;
#7743=CARTESIAN_POINT ( 'NONE',  ( -3.458734125000000770, 1.432654583217640498, 0.9250000013655965692 ) ) ;
#7749=CARTESIAN_POINT ( 'NONE',  ( -3.458734125000000770, 1.432654583217640498, 4.925000001365594571 ) ) ;
#7780=CARTESIAN_POINT ( 'NONE',  ( -1.876855952934450622, 6.421950209808279908, -0.1061556211655337173 ) ) ;
#7785=CONICAL_SURFACE ( 'NONE', #21527, 6.500000000000000888, 1.047197551196596521 ) ;
#7798=CARTESIAN_POINT ( 'NONE',  ( 6.500000000000000000, 0.6345343291280540754, -3.700000000000000178 ) ) ;
#7802=VECTOR ( 'NONE', #2080, 1000.000000000000000 ) ;
#7803=CARTESIAN_POINT ( 'NONE',  ( 3.250000000000001776, -5.629165124598848990, 1.734723475976807094E-15 ) ) ;
#7808=CARTESIAN_POINT ( 'NONE',  ( -3.458734125000000770, 0.000000000000000000, -1.012499998634402543 ) ) ;
#7809=CARTESIAN_POINT ( 'NONE',  ( 1.656854249492383024, -3.999999999999999112, 0.6125000000000022649 ) ) ;
#7831=CARTESIAN_POINT ( 'NONE',  ( 4.000000000000000000, 0.000000000000000000, 19.04999999999996874 ) ) ;
#7832=CARTESIAN_POINT ( 'NONE',  ( -2.117863837641485618E-16, 3.458734125000000770, 2.737500001365597235 ) ) ;
#7840=CARTESIAN_POINT ( 'NONE',  ( 1.432654583217639832, 3.458734125000000326, 3.425000001365596791 ) ) ;
#7850=CARTESIAN_POINT ( 'NONE',  ( 3.458734125000000770, 1.432654583217640498, -1.449999998634403875 ) ) ;
#7858=CARTESIAN_POINT ( 'NONE',  ( -2.445694354108820523, 2.445694354108820523, 3.862500001365594571 ) ) ;
#7866=CARTESIAN_POINT ( 'NONE',  ( -4.000000000000000000, 0.000000000000000000, 4.425000002731186655 ) ) ;
#7906=CARTESIAN_POINT ( 'NONE',  ( 1.656854249492383024, -3.999999999999999112, 1.612500000000001377 ) ) ;
#7917=FACE_OUTER_BOUND ( 'NONE', #17457, .T. ) ;
#7922=CARTESIAN_POINT ( 'NONE',  ( -2.828427124746190291, 2.828427124746190291, 3.175000000000002487 ) ) ;
#7926=DIRECTION ( 'NONE',  ( 0.000000000000000000, -0.000000000000000000, 1.000000000000000000 ) ) ;
#7952=CARTESIAN_POINT ( 'NONE',  ( 6.353591512924457348E-16, -3.458734125000000770, 5.237500001365596347 ) ) ;
#7962=CARTESIAN_POINT ( 'NONE',  ( -2.117863837641485618E-16, 3.458734125000000326, 2.487500001365596791 ) ) ;
#7964=CARTESIAN_POINT ( 'NONE',  ( -2.445694354108819635, -2.445694354108820523, -0.1374999986344035974 ) ) ;
#7967=EDGE_CURVE ( 'NONE', #20452, #19427, #1727, .T. ) ;
#7971=ORIENTED_EDGE ( 'NONE', *, *, #18837, .T. ) ;
#7983=CARTESIAN_POINT ( 'NONE',  ( 2.445694354108820079, 2.445694354108820523, 5.612500001365596347 ) ) ;
#7988=FACE_OUTER_BOUND ( 'NONE', #13994, .T. ) ;
#7991=CARTESIAN_POINT ( 'NONE',  ( 1.656854249492383024, -3.999999999999999112, 3.737500002731185766 ) ) ;
#7994=ORIENTED_EDGE ( 'NONE', *, *, #2231, .T. ) ;
#8010=CARTESIAN_POINT ( 'NONE',  ( -1.647987302177966740E-14, -7.505553499465137612, -3.119443416399232394 ) ) ;
#8037=CARTESIAN_POINT ( 'NONE',  ( 3.250000000000004441, 5.629165124598849879, -3.700000000000000178 ) ) ;
#8041=AXIS2_PLACEMENT_3D ( 'NONE', #14757, #5276, #16310 ) ;
#8051=CARTESIAN_POINT ( 'NONE',  ( 0.000000000000000000, 0.000000000000000000, 0.000000000000000000 ) ) ;
#8053=CARTESIAN_POINT ( 'NONE',  ( 2.828427124746189847, 2.828427124746190291, 0.9250000000000004885 ) ) ;
#8064=CARTESIAN_POINT ( 'NONE',  ( 2.828427124746189847, 2.828427124746190291, -1.949999997268811791 ) ) ;
#8065=VERTEX_POINT ( 'NONE', #3533 ) ;
#8083=CARTESIAN_POINT ( 'NONE',  ( 6.353591512924457348E-16, -3.458734125000000770, 4.237500001365595459 ) ) ;
#8087=CIRCLE ( 'NONE', #21426, 6.500000000000000888 ) ;
#8092=CARTESIAN_POINT ( 'NONE',  ( 6.353591512924457348E-16, -3.458734125000000326, 0.9875000013655956810 ) ) ;
#8093=CARTESIAN_POINT ( 'NONE',  ( 6.353591512924457348E-16, -3.458734125000000326, -1.012499998634402543 ) ) ;
#8096=( NAMED_UNIT ( * ) SI_UNIT ( $, .STERADIAN. ) SOLID_ANGLE_UNIT ( ) );
#8102=CARTESIAN_POINT ( 'NONE',  ( 2.445694354108820967, -2.445694354108820079, -2.637499998634404097 ) ) ;
#8103=AXIS2_PLACEMENT_3D ( 'NONE', #4905, #12719, #1407 ) ;
#8104=CARTESIAN_POINT ( 'NONE',  ( -3.250000000000004885, -5.629165124598848990, -3.700000000000000178 ) ) ;
#8106=DIRECTION ( 'NONE',  ( 1.000000000000000000, 0.000000000000000000, 0.000000000000000000 ) ) ;
#8112=CARTESIAN_POINT ( 'NONE',  ( -3.458734125000000326, 0.000000000000000000, -2.262499998634403653 ) ) ;
#8139=VERTEX_POINT ( 'NONE', #4472 ) ;
#8150=CARTESIAN_POINT ( 'NONE',  ( 2.828427124746189847, 2.828427124746190291, 0.9250000000000004885 ) ) ;
#8160=CARTESIAN_POINT ( 'NONE',  ( 3.250000000000003109, 5.629165124598848102, 1.734723475976807094E-15 ) ) ;
#8166=CARTESIAN_POINT ( 'NONE',  ( -2.828427124746189403, -2.828427124746190735, 0.4250000000000017653 ) ) ;
#8191=CARTESIAN_POINT ( 'NONE',  ( -3.458734125000000326, -1.432654583217642497, 2.050000001365597679 ) ) ;
#8198=ORIENTED_EDGE ( 'NONE', *, *, #11437, .F. ) ;
#8200=CARTESIAN_POINT ( 'NONE',  ( 2.445694354108820523, -2.445694354108820079, 0.1125000013655966247 ) ) ;
#8201=EDGE_CURVE ( 'NONE', #7525, #3785, #9535, .T. ) ;
#8207=ORIENTED_EDGE ( 'NONE', *, *, #15076, .T. ) ;
#8211=CONICAL_SURFACE ( 'NONE', #143, 6.500000000000000888, 1.047197551196596521 ) ;
#8221=CARTESIAN_POINT ( 'NONE',  ( -3.458734125000000770, 0.000000000000000000, 4.987500001365595459 ) ) ;
#8230=CARTESIAN_POINT ( 'NONE',  ( 4.000000000000000000, 4.898587196589412829E-16, 2.925000002731188875 ) ) ;
#8251=DIRECTION ( 'NONE',  ( -0.000000000000000000, -0.000000000000000000, 1.000000000000000000 ) ) ;
#8257=CARTESIAN_POINT ( 'NONE',  ( -4.000000000000000000, 0.000000000000000000, -1.699999999999998401 ) ) ;
#8283=CARTESIAN_POINT ( 'NONE',  ( -1.656854249492380804, 4.000000000000000000, -1.887499999999998179 ) ) ;
#8288=ORIENTED_EDGE ( 'NONE', *, *, #11437, .T. ) ;
#8303=CARTESIAN_POINT ( 'NONE',  ( 2.445694354108820967, -2.445694354108820079, 5.362500001365596347 ) ) ;
#8311=DIRECTION ( 'NONE',  ( 0.000000000000000000, 0.000000000000000000, 1.000000000000000000 ) ) ;
#8319=B_SPLINE_CURVE_WITH_KNOTS ( 'NONE', 3,
 ( #23072, #7160, #21621, #12212, #3312, #17703 ),
 .UNSPECIFIED., .F., .F.,
 ( 4, 2, 4 ),
 ( 0.01049192114530184475, 0.01239128608052813933, 0.01429065101575443392 ),
 .UNSPECIFIED. ) ;
#8322=CARTESIAN_POINT ( 'NONE',  ( -2.117863837641485618E-16, 3.458734125000000770, -2.262499998634403653 ) ) ;
#8337=CARTESIAN_POINT ( 'NONE',  ( -1.432654583217640498, 3.458734125000000770, 2.800000001365598123 ) ) ;
#8346=CARTESIAN_POINT ( 'NONE',  ( 7.347880794884118750E-16, -4.000000000000000000, 3.675000002731186211 ) ) ;
#8365=CARTESIAN_POINT ( 'NONE',  ( 1.432654583217639832, 3.458734125000000326, 4.425000001365595459 ) ) ;
#8373=ORIENTED_EDGE ( 'NONE', *, *, #5901, .F. ) ;
#8381=ORIENTED_EDGE ( 'NONE', *, *, #5901, .T. ) ;
#8387=CARTESIAN_POINT ( 'NONE',  ( -5.432802636760778903, 4.368923434677189910, -0.2573354458087841468 ) ) ;
#8389=LINE ( 'NONE', #11879, #15624 ) ;
#8395=AXIS2_PLACEMENT_3D ( 'NONE', #21432, #5162, #1677 ) ;
#8402=DIRECTION ( 'NONE',  ( -0.000000000000000000, 0.000000000000000000, -1.000000000000000000 ) ) ;
#8405=CARTESIAN_POINT ( 'NONE',  ( -2.828427124746190291, 2.828427124746190291, -0.8249999999999976241 ) ) ;
#8406=B_SPLINE_CURVE_WITH_KNOTS ( 'NONE', 3,
 ( #314, #1755, #9439, #19839, #3445, #1869 ),
 .UNSPECIFIED., .F., .F.,
 ( 4, 2, 4 ),
 ( 0.006695446894088488872, 0.008593684019695166376, 0.01049192114530184301 ),
 .UNSPECIFIED. ) ;
#8417=ORIENTED_EDGE ( 'NONE', *, *, #7967, .T. ) ;
#8418=CARTESIAN_POINT ( 'NONE',  ( 1.656854249492380138, 4.000000000000000000, -1.887499997268811791 ) ) ;
#8422=CIRCLE ( 'NONE', #19094, 4.714285714285714413 ) ;
#8423=DIRECTION ( 'NONE',  ( 0.000000000000000000, 0.000000000000000000, -1.000000000000000000 ) ) ;
#8433=CARTESIAN_POINT ( 'NONE',  ( 3.458734125000000770, 4.235727675282972223E-16, 1.487500001365596125 ) ) ;
#8445=CARTESIAN_POINT ( 'NONE',  ( 1.432654583217639832, 3.458734125000000326, 1.425000001365597013 ) ) ;
#8448=DIRECTION ( 'NONE',  ( 1.000000000000000000, 0.000000000000000000, 0.000000000000000000 ) ) ;
#8451=ORIENTED_EDGE ( 'NONE', *, *, #13190, .T. ) ;
#8466=CARTESIAN_POINT ( 'NONE',  ( 6.353591512924457348E-16, -3.458734125000000770, 3.237500001365597679 ) ) ;
#8468=CARTESIAN_POINT ( 'NONE',  ( -6.500000000000000000, -3.752776749732572359, -3.700000000000000178 ) ) ;
#8475=CARTESIAN_POINT ( 'NONE',  ( 1.656854249492383024, -3.999999999999999112, 1.737500002731187543 ) ) ;
#8490=CARTESIAN_POINT ( 'NONE',  ( -3.458734125000000326, 1.432654583217640276, 3.675000001365593238 ) ) ;
#8502=EDGE_CURVE ( 'NONE', #12637, #20551, #21820, .T. ) ;
#8521=CARTESIAN_POINT ( 'NONE',  ( -1.656854249492381248, -3.999999999999999112, -2.512499999999998401 ) ) ;
#8523=CARTESIAN_POINT ( 'NONE',  ( 2.828427124746190735, -2.828427124746189847, 0.8000000027311872097 ) ) ;
#8529=CARTESIAN_POINT ( 'NONE',  ( -6.500000000000000000, 0.000000000000000000, 1.734723475976807094E-15 ) ) ;
#8533=ORIENTED_EDGE ( 'NONE', *, *, #11760, .T. ) ;
#8543=CARTESIAN_POINT ( 'NONE',  ( -3.458734125000000326, -1.432654583217642497, 1.050000001365596791 ) ) ;
#8547=DIRECTION ( 'NONE',  ( -1.000000000000000000, -8.881784197001252323E-16, 0.000000000000000000 ) ) ;
#8552=CARTESIAN_POINT ( 'NONE',  ( -1.432654583217640276, 3.458734125000000326, -1.449999998634403875 ) ) ;
#8554=CARTESIAN_POINT ( 'NONE',  ( 0.000000000000000000, 0.000000000000000000, 19.04999999999996874 ) ) ;
#8564=CARTESIAN_POINT ( 'NONE',  ( -4.714285714285714413, 5.773334910266094008E-16, 9.480888224575631185 ) ) ;
#8571=CARTESIAN_POINT ( 'NONE',  ( -2.445694354108820523, 2.445694354108820523, 1.862500001365596347 ) ) ;
#8578=VERTEX_POINT ( 'NONE', #6346 ) ;
#8581=CARTESIAN_POINT ( 'NONE',  ( 2.828427124746190735, -2.828427124746189847, -1.199999997268811125 ) ) ;
#8584=CARTESIAN_POINT ( 'NONE',  ( 0.5303295852573084446, -7.199367570657613236, -0.4037800551813831573 ) ) ;
#8594=AXIS2_PLACEMENT_3D ( 'NONE', #6302, #22581, #6660 ) ;
#8597=CARTESIAN_POINT ( 'NONE',  ( -2.117863837641485618E-16, 3.458734125000000326, 5.487500001365596347 ) ) ;
#8621=ADVANCED_FACE ( 'NONE', ( #5093 ), #22437, .F. ) ;
#8629=CARTESIAN_POINT ( 'NONE',  ( -6.500000000000000000, -3.752776749732573247, -3.119443416399232394 ) ) ;
#8638=CARTESIAN_POINT ( 'NONE',  ( -1.432654583217640942, -3.458734124999999882, -0.07499999863440427739 ) ) ;
#8642=ORIENTED_EDGE ( 'NONE', *, *, #16405, .T. ) ;
#8647=AXIS2_PLACEMENT_3D ( 'NONE', #23025, #15754, #8311 ) ;
#8658=CARTESIAN_POINT ( 'NONE',  ( -3.458734125000000770, 1.432654583217640498, 0.9250000013655964581 ) ) ;
#8671=CARTESIAN_POINT ( 'NONE',  ( -1.432654583217640942, -3.458734124999999882, -3.074999998634404985 ) ) ;
#8674=ORIENTED_EDGE ( 'NONE', *, *, #6695, .F. ) ;
#8687=CARTESIAN_POINT ( 'NONE',  ( 3.458734125000000770, 1.432654583217640498, 2.550000001365598123 ) ) ;
#8697=CARTESIAN_POINT ( 'NONE',  ( -2.449293598294706907E-16, 4.000000000000000000, 0.1750000027311865991 ) ) ;
#8714=CARTESIAN_POINT ( 'NONE',  ( 3.458734125000000770, -1.432654583217639610, 2.175000001365597679 ) ) ;
#8719=CARTESIAN_POINT ( 'NONE',  ( -3.058823393344586528, 2.118763015513301262, 2.039999999999997815 ) ) ;
#8723=AXIS2_PLACEMENT_3D ( 'NONE', #20666, #16860, #794 ) ;
#8740=MECHANICAL_DESIGN_GEOMETRIC_PRESENTATION_REPRESENTATION('',(#9898),#19816);
#8749=CARTESIAN_POINT ( 'NONE',  ( -3.381512639161500466, 0.7267833367865139671, -3.295601554149589330 ) ) ;
#8755=CARTESIAN_POINT ( 'NONE',  ( -2.366436158131400969E-16, 3.864683531250000303, -3.028124999658599048 ) ) ;
#8756=CARTESIAN_POINT ( 'NONE',  ( 1.432654583217642275, -3.458734124999999437, -0.9499999986344030978 ) ) ;
#8778=CARTESIAN_POINT ( 'NONE',  ( -1.432654583217640498, 3.458734125000000770, -2.199999998634404541 ) ) ;
#8785=VERTEX_POINT ( 'NONE', #16477 ) ;
#8790=ADVANCED_BREP_SHAPE_REPRESENTATION ( '', ( #6915, #7318 ), #9900 ) ;
#8793=CARTESIAN_POINT ( 'NONE',  ( 1.432654583217642053, -3.458734124999999437, -1.949999998634404097 ) ) ;
#8816=CARTESIAN_POINT ( 'NONE',  ( -2.445694354108819635, -2.445694354108820967, 3.112500001365597679 ) ) ;
#8817=CARTESIAN_POINT ( 'NONE',  ( 0.01183343685760930748, -3.466145975376039079, 2.040000000000000036 ) ) ;
#8821=DIRECTION ( 'NONE',  ( -0.000000000000000000, 0.000000000000000000, -1.000000000000000000 ) ) ;
#8826=CARTESIAN_POINT ( 'NONE',  ( 4.000000000000000000, 4.898587196589412829E-16, -0.07499999726881187434 ) ) ;
#8831=CARTESIAN_POINT ( 'NONE',  ( 4.332341089154587834E-16, 7.505553499465137612, -3.700000000000000178 ) ) ;
#8845=DIRECTION ( 'NONE',  ( -0.000000000000000000, -0.000000000000000000, 1.000000000000000000 ) ) ;
#8885=CARTESIAN_POINT ( 'NONE',  ( -3.458734125000000326, 0.000000000000000000, -0.2624999986344037084 ) ) ;
#8894=DIRECTION ( 'NONE',  ( -0.000000000000000000, -0.000000000000000000, 1.000000000000000000 ) ) ;
#8901=CARTESIAN_POINT ( 'NONE',  ( 1.432654583217642275, -3.458734124999999882, -0.6999999986344028757 ) ) ;
#8914=CARTESIAN_POINT ( 'NONE',  ( -2.445694354108819635, -2.445694354108820523, -2.137499998634403653 ) ) ;
#8925=DIRECTION ( 'NONE',  ( -0.000000000000000000, 0.000000000000000000, -1.000000000000000000 ) ) ;
#8927=CARTESIAN_POINT ( 'NONE',  ( -1.656854249492381248, -3.999999999999999112, -2.387499997268812013 ) ) ;
#8933=CARTESIAN_POINT ( 'NONE',  ( 1.432654583217640276, 3.458734125000000770, -1.324999998634403653 ) ) ;
#8934=DIRECTION ( 'NONE',  ( -1.000000000000000000, 0.000000000000000000, 0.000000000000000000 ) ) ;
#8943=CARTESIAN_POINT ( 'NONE',  ( 4.000000000000000000, 4.898587196589412829E-16, -1.074999997268812679 ) ) ;
#8956=EDGE_LOOP ( 'NONE', ( #7261, #6086 ) ) ;
#8962=CARTESIAN_POINT ( 'NONE',  ( -6.499999999999999112, 7.960204194457795477E-16, 2.040000000000001812 ) ) ;
#8965=CARTESIAN_POINT ( 'NONE',  ( 2.445694354108820079, 2.445694354108820523, -0.6374999986344040970 ) ) ;
#8968=CARTESIAN_POINT ( 'NONE',  ( -4.000000000000000888, 1.656854249492380582, 0.2375000000000018763 ) ) ;
#8991=ORIENTED_EDGE ( 'NONE', *, *, #6606, .T. ) ;
#8999=CARTESIAN_POINT ( 'NONE',  ( -1.515948947685982429, 3.114950916665994995, -3.295601554149324208 ) ) ;
#9003=ADVANCED_FACE ( 'NONE', ( #1556 ), #18350, .T. ) ;
#9007=CARTESIAN_POINT ( 'NONE',  ( 3.458734125000000770, -1.432654583217639610, -1.824999998634404097 ) ) ;
#9014=APPLICATION_CONTEXT ( 'automotive_design' ) ;
#9017=CARTESIAN_POINT ( 'NONE',  ( 0.000000000000000000, 0.000000000000000000, 3.059999999999998277 ) ) ;
#9024=CARTESIAN_POINT ( 'NONE',  ( -1.656854249492380804, 4.000000000000000000, 4.112500000000001599 ) ) ;
#9025=CARTESIAN_POINT ( 'NONE',  ( -4.000000000000000000, 0.000000000000000000, 0.3000000000000016542 ) ) ;
#9034=CARTESIAN_POINT ( 'NONE',  ( -2.445694354108820523, 2.445694354108820523, -1.387499998634402987 ) ) ;
#9050=CARTESIAN_POINT ( 'NONE',  ( -2.272871948086449656, -2.616781258933798426, 2.039999999999998259 ) ) ;
#9058=CARTESIAN_POINT ( 'NONE',  ( -4.000000000000000000, -1.656854249492383246, -3.512499997268812901 ) ) ;
#9077=CARTESIAN_POINT ( 'NONE',  ( 3.458734125000000770, -1.432654583217639610, 1.175000001365597013 ) ) ;
#9121=VECTOR ( 'NONE', #2305, 1000.000000000000000 ) ;
#9126=ORIENTED_EDGE ( 'NONE', *, *, #12196, .F. ) ;
#9145=CARTESIAN_POINT ( 'NONE',  ( 2.445694354108820079, 2.445694354108820523, -2.387499998634403653 ) ) ;
#9148=DIRECTION ( 'NONE',  ( 0.000000000000000000, 0.000000000000000000, 1.000000000000000000 ) ) ;
#9149=ORIENTED_EDGE ( 'NONE', *, *, #11134, .T. ) ;
#9150=CIRCLE ( 'NONE', #17111, 6.500000000000000888 ) ;
#9165=ADVANCED_FACE ( 'NONE', ( #6967 ), #11043, .T. ) ;
#9174=CARTESIAN_POINT ( 'NONE',  ( 0.2373759324227673606, -3.458017446235651438, 2.039999999999998259 ) ) ;
#9183=CARTESIAN_POINT ( 'NONE',  ( -2.117863837641485618E-16, 3.458734125000000326, 4.487500001365595459 ) ) ;
#9194=CARTESIAN_POINT ( 'NONE',  ( -2.117863837641485618E-16, 3.458734125000000770, -0.2624999986344037084 ) ) ;
#9201=CARTESIAN_POINT ( 'NONE',  ( 2.445694354108820523, -2.445694354108820079, -1.887499998634403431 ) ) ;
#9210=EDGE_LOOP ( 'NONE', ( #5181, #8642, #21349, #2121 ) ) ;
#9224=CARTESIAN_POINT ( 'NONE',  ( 0.000000000000000000, 0.000000000000000000, 2.040000000000001812 ) ) ;
#9235=CARTESIAN_POINT ( 'NONE',  ( 0.000000000000000000, 0.000000000000000000, -3.700000000000000178 ) ) ;
#9240=CARTESIAN_POINT ( 'NONE',  ( -4.000000000000000000, 0.000000000000000000, -3.574999997268813345 ) ) ;
#9241=CARTESIAN_POINT ( 'NONE',  ( -3.458734124999999882, -1.432654583217642497, -0.1999999986344043745 ) ) ;
#9243=EDGE_CURVE ( 'NONE', #3610, #10634, #21909, .T. ) ;
#9261=CARTESIAN_POINT ( 'NONE',  ( 1.656854249492380360, 4.000000000000000000, 5.987500000000000711 ) ) ;
#9274=ADVANCED_FACE ( 'NONE', ( #22495 ), #3422, .T. ) ;
#9290=ORIENTED_EDGE ( 'NONE', *, *, #12659, .T. ) ;
#9293=CARTESIAN_POINT ( 'NONE',  ( -4.000000000000000000, -1.656854249492383246, -2.512499997268812457 ) ) ;
#9301=ORIENTED_EDGE ( 'NONE', *, *, #10543, .T. ) ;
#9309=CARTESIAN_POINT ( 'NONE',  ( 6.353591512924457348E-16, -3.458734125000000326, -1.012499998634402543 ) ) ;
#9320=ORIENTED_EDGE ( 'NONE', *, *, #7147, .F. ) ;
#9322=EDGE_LOOP ( 'NONE', ( #9415, #18413, #12386, #787, #4602, #21294 ) ) ;
#9342=CARTESIAN_POINT ( 'NONE',  ( 3.803704290982252711, -5.309483803148803638, -3.700000000000000622 ) ) ;
#9355=FACE_OUTER_BOUND ( 'NONE', #6987, .T. ) ;
#9358=ADVANCED_FACE ( 'NONE', ( #227 ), #4065, .F. ) ;
#9365=DIRECTION ( 'NONE',  ( -0.000000000000000000, -0.000000000000000000, 1.000000000000000000 ) ) ;
#9372=CARTESIAN_POINT ( 'NONE',  ( -3.458734125000000770, 1.432654583217640498, -3.074999998634403209 ) ) ;
#9384=EDGE_CURVE ( 'NONE', #18029, #12600, #13093, .T. ) ;
#9396=DIRECTION ( 'NONE',  ( -0.000000000000000000, -0.000000000000000000, 1.000000000000000000 ) ) ;
#9398=FACE_OUTER_BOUND ( 'NONE', #20826, .T. ) ;
#9408=CARTESIAN_POINT ( 'NONE',  ( 3.458734125000000326, 4.235727675282971730E-16, 5.237500001365596347 ) ) ;
#9415=ORIENTED_EDGE ( 'NONE', *, *, #22504, .T. ) ;
#9418=CARTESIAN_POINT ( 'NONE',  ( -2.117863837641485618E-16, 3.458734125000000770, 0.7375000013655954589 ) ) ;
#9423=EDGE_CURVE ( 'NONE', #15256, #10924, #8422, .T. ) ;
#9424=DIRECTION ( 'NONE',  ( -5.015859645267662560E-17, 0.8191520442889899112, -0.5735764363510487129 ) ) ;
#9426=CARTESIAN_POINT ( 'NONE',  ( -3.458734125000000326, 1.432654583217640276, -1.324999998634403653 ) ) ;
#9436=DIRECTION ( 'NONE',  ( 1.000000000000000000, 0.000000000000000000, 0.000000000000000000 ) ) ;
#9439=CARTESIAN_POINT ( 'NONE',  ( -6.500000000000002665, -2.517290933526016961, -0.2565799252183981749 ) ) ;
#9448=DIRECTION ( 'NONE',  ( -0.000000000000000000, -0.000000000000000000, 1.000000000000000000 ) ) ;
#9474=CARTESIAN_POINT ( 'NONE',  ( 0.5316568767328667677, 7.198601258566900363, -3.296662375310746462 ) ) ;
#9483=CARTESIAN_POINT ( 'NONE',  ( -1.432654583217640498, 3.458734125000000770, -3.199999998634403209 ) ) ;
#9484=CARTESIAN_POINT ( 'NONE',  ( 1.656854249492383024, -3.999999999999999112, 1.612500000000001377 ) ) ;
#9490=EDGE_CURVE ( 'NONE', #14307, #669, #6788, .T. ) ;
#9506=AXIS2_PLACEMENT_3D ( 'NONE', #11077, #9396, #22293 ) ;
#9516=CONICAL_SURFACE ( 'NONE', #22473, 6.500000000000000888, 1.047197551196596521 ) ;
#9522=VERTEX_POINT ( 'NONE', #17718 ) ;
#9528=CARTESIAN_POINT ( 'NONE',  ( 1.656854249492380360, 4.000000000000000000, -1.887499997268811791 ) ) ;
#9535=LINE ( 'NONE', #9891, #23244 ) ;
#9542=CARTESIAN_POINT ( 'NONE',  ( 2.445694354108820967, -2.445694354108820079, 1.362500001365595903 ) ) ;
#9544=CARTESIAN_POINT ( 'NONE',  ( -1.876855952934450622, 6.421950209808279908, -3.593844378834467612 ) ) ;
#9548=CARTESIAN_POINT ( 'NONE',  ( 2.445694354108820079, 2.445694354108820523, 4.612500001365595459 ) ) ;
#9579=CARTESIAN_POINT ( 'NONE',  ( -1.656854249492380582, 4.000000000000000000, 0.2375000027311863493 ) ) ;
#9587=CARTESIAN_POINT ( 'NONE',  ( 5.432802636760778903, -4.368923434677197903, -3.442664554191212201 ) ) ;
#9598=CARTESIAN_POINT ( 'NONE',  ( -2.449293598294706907E-16, 4.000000000000000000, -2.949999999999997957 ) ) ;
#9600=CARTESIAN_POINT ( 'NONE',  ( -2.449293598294706907E-16, 4.000000000000000000, 1.050000000000000488 ) ) ;
#9617=CARTESIAN_POINT ( 'NONE',  ( 2.445694354108820967, -2.445694354108820079, -0.6374999986344023206 ) ) ;
#9618=CARTESIAN_POINT ( 'NONE',  ( 7.347880794884118750E-16, -4.000000000000000000, 1.550000000000000933 ) ) ;
#9632=ORIENTED_EDGE ( 'NONE', *, *, #6606, .F. ) ;
#9642=CARTESIAN_POINT ( 'NONE',  ( 1.432654583217640276, 3.458734125000000770, 5.675000001365596347 ) ) ;
#9651=SURFACE_STYLE_FILL_AREA ( #4238 ) ;
#9652=CARTESIAN_POINT ( 'NONE',  ( -3.458734125000000326, 1.432654583217640276, 3.675000001365593238 ) ) ;
#9664=ADVANCED_FACE ( 'NONE', ( #14256 ), #20247, .T. ) ;
#9668=CARTESIAN_POINT ( 'NONE',  ( 2.445694354108820967, -2.445694354108820079, 4.362500001365595459 ) ) ;
#9726=CARTESIAN_POINT ( 'NONE',  ( -2.117863837641485618E-16, 3.458734125000000770, -2.262499998634403653 ) ) ;
#9727=CARTESIAN_POINT ( 'NONE',  ( 2.828427124746189847, 2.828427124746190291, 1.925000000000001377 ) ) ;
#9728=CARTESIAN_POINT ( 'NONE',  ( -4.000000000000000000, -1.656854249492383024, -3.512499997268813345 ) ) ;
#9738=( BOUNDED_CURVE ( )  B_SPLINE_CURVE ( 2, ( #4594, #2897, #6633, #21206, #6278, #22905, #9887, #19198, #21095, #13950, #20747, #8445, #4708, #986, #22667, #4821, #17302, #17181, #15404, #10014, #1100, #18844, #4352, #6519, #20861, #10243, #19304, #6163, #22555, #13712, #2430, #12040, #17533, #2783, #17061, #11689, #7964, #15283, #13485, #866, #11932, #10124, #2672, #4467, #2542, #15516, #13839, #22785, #761, #20975, #8093, #11808, #19080, #17417, #6392, #15635, #9034, #8552, #10838, #17878, #21563, #12517, #19657, #6864, #21324, #8793, #7107, #16095, #8914, #6984, #16327, #1452, #23493, #3258, #23382, #21447, #23620, #12279, #19900, #17998, #3502, #1576, #5299, #8671, #17763, #14550, #5059, #12392, #14424 ),
 .UNSPECIFIED., .F., .F. ) 
 B_SPLINE_CURVE_WITH_KNOTS ( ( 3, 2, 2, 2, 2, 2, 2, 2, 2, 2, 2, 2, 2, 2, 2, 2, 2, 2, 2, 2, 2, 2, 2, 2, 2, 2, 2, 2, 2, 2, 2, 2, 2, 2, 2, 2, 2, 2, 2, 2, 2, 2, 2, 2, 3 ),
 ( 0.3697128431780269953, 0.3750000000000000000, 0.3875000000000000111, 0.4000000000000000222, 0.4124999999999999778, 0.4249999999999999889, 0.4375000000000000000, 0.4500000000000000111, 0.4625000000000000222, 0.4749999999999999778, 0.4874999999999999889, 0.5000000000000000000, 0.5124999999999999556, 0.5250000000000000222, 0.5374999999999999778, 0.5500000000000000444, 0.5625000000000000000, 0.5749999999999999556, 0.5875000000000000222, 0.5999999999999999778, 0.6125000000000000444, 0.6250000000000000000, 0.6374999999999999556, 0.6500000000000000222, 0.6624999999999999778, 0.6750000000000000444, 0.6875000000000000000, 0.6999999999999999556, 0.7125000000000000222, 0.7249999999999999778, 0.7375000000000000444, 0.7500000000000000000, 0.7624999999999999556, 0.7750000000000000222, 0.7874999999999999778, 0.8000000000000000444, 0.8125000000000000000, 0.8249999999999999556, 0.8375000000000000222, 0.8499999999999999778, 0.8625000000000000444, 0.8750000000000000000, 0.8874999999999999556, 0.9000000000000000222, 0.9033987602710955578 ),
 .UNSPECIFIED. ) 
 CURVE ( )  GEOMETRIC_REPRESENTATION_ITEM ( )  RATIONAL_B_SPLINE_CURVE ( ( 0.9628430465414361539, 0.9678031320820220662, 1.000000000000000000, 0.9238795325112867385, 1.000000000000000000, 0.9238795325112867385, 1.000000000000000000, 0.9238795325112867385, 1.000000000000000000, 0.9238795325112867385, 1.000000000000000000, 0.9238795325112867385, 1.000000000000000000, 0.9238795325112867385, 1.000000000000000000, 0.9238795325112867385, 1.000000000000000000, 0.9238795325112867385, 1.000000000000000000, 0.9238795325112867385, 1.000000000000000000, 0.9238795325112867385, 1.000000000000000000, 0.9238795325112867385, 1.000000000000000000, 0.9238795325112867385, 1.000000000000000000, 0.9238795325112867385, 1.000000000000000000, 0.9238795325112867385, 1.000000000000000000, 0.9238795325112867385, 1.000000000000000000, 0.9238795325112867385, 1.000000000000000000, 0.9238795325112867385, 1.000000000000000000, 0.9238795325112867385, 1.000000000000000000, 0.9238795325112867385, 1.000000000000000000, 0.9238795325112867385, 1.000000000000000000, 0.9238795325112867385, 1.000000000000000000, 0.9238795325112867385, 1.000000000000000000, 0.9238795325112867385, 1.000000000000000000, 0.9238795325112867385, 1.000000000000000000, 0.9238795325112867385, 1.000000000000000000, 0.9238795325112867385, 1.000000000000000000, 0.9238795325112867385, 1.000000000000000000, 0.9238795325112867385, 1.000000000000000000, 0.9238795325112867385, 1.000000000000000000, 0.9238795325112867385, 1.000000000000000000, 0.9238795325112867385, 1.000000000000000000, 0.9238795325112867385, 1.000000000000000000, 0.9238795325112867385, 1.000000000000000000, 0.9238795325112867385, 1.000000000000000000, 0.9238795325112867385, 1.000000000000000000, 0.9238795325112867385, 1.000000000000000000, 0.9238795325112867385, 1.000000000000000000, 0.9238795325112867385, 1.000000000000000000, 0.9238795325112867385, 1.000000000000000000, 0.9238795325112867385, 1.000000000000000000, 0.9238795325112867385, 1.000000000000000000, 0.9238795325112867385, 1.000000000000000000, 0.9793027823425712874, 0.9698607456605483623 ) ) 
 REPRESENTATION_ITEM ( '' )  );
#9739=VERTEX_POINT ( 'NONE', #6073 ) ;
#9740=CARTESIAN_POINT ( 'NONE',  ( -4.000000000000000000, 0.000000000000000000, -1.574999997268811569 ) ) ;
#9751=CARTESIAN_POINT ( 'NONE',  ( -3.458734125000000770, 0.000000000000000000, 1.987500001365596569 ) ) ;
#9759=CARTESIAN_POINT ( 'NONE',  ( -2.117863837641485618E-16, 3.458734125000000326, 1.487500001365596125 ) ) ;
#9761=PLANE ( 'NONE',  #8647 ) ;
#9781=CARTESIAN_POINT ( 'NONE',  ( -1.432654583217640942, -3.458734124999999882, -2.074999998634404097 ) ) ;
#9785=CARTESIAN_POINT ( 'NONE',  ( -2.449293598294706907E-16, 4.000000000000000000, -1.949999999999998623 ) ) ;
#9788=CARTESIAN_POINT ( 'NONE',  ( 2.828427124746189847, 2.828427124746190291, 4.050000002731186655 ) ) ;
#9793=CARTESIAN_POINT ( 'NONE',  ( -4.000000000000000000, 0.000000000000000000, 1.425000002731187765 ) ) ;
#9806=CARTESIAN_POINT ( 'NONE',  ( 4.000000000000000000, 4.898587196589412829E-16, -0.07499999726881187434 ) ) ;
#9814=ORIENTED_EDGE ( 'NONE', *, *, #20323, .F. ) ;
#9834=DIRECTION ( 'NONE',  ( -1.000000000000000000, 0.000000000000000000, 0.000000000000000000 ) ) ;
#9844=CARTESIAN_POINT ( 'NONE',  ( -4.000000000000000000, 0.000000000000000000, 3.300000000000002487 ) ) ;
#9854=EDGE_CURVE ( 'NONE', #9739, #20452, #22853, .T. ) ;
#9873=( BOUNDED_CURVE ( )  B_SPLINE_CURVE ( 2, ( #10555, #16392, #85, #12465, #12348, #3675, #12817, #17829, #1396 ),
 .UNSPECIFIED., .F., .F. ) 
 B_SPLINE_CURVE_WITH_KNOTS ( ( 3, 2, 2, 2, 3 ),
 ( 0.6500000000000000222, 0.6624999999999999778, 0.6750000000000000444, 0.6875000000000000000, 0.6999999999999999556 ),
 .UNSPECIFIED. ) 
 CURVE ( )  GEOMETRIC_REPRESENTATION_ITEM ( )  RATIONAL_B_SPLINE_CURVE ( ( 1.000000000000000000, 0.9238795325112867385, 1.000000000000000000, 0.9238795325112867385, 1.000000000000000000, 0.9238795325112867385, 1.000000000000000000, 0.9238795325112867385, 1.000000000000000000 ) ) 
 REPRESENTATION_ITEM ( '' )  );
#9874=CARTESIAN_POINT ( 'NONE',  ( -3.458734125000000326, -1.432654583217642497, 4.050000001365596347 ) ) ;
#9877=B_SPLINE_CURVE_WITH_KNOTS ( 'NONE', 3,
 ( #21729, #3540, #14820, #14946, #9544, #10875, #20044, #1735 ),
 .UNSPECIFIED., .F., .F.,
 ( 4, 2, 2, 4 ),
 ( 0.003797433802554438069, 0.004743183970586236156, 0.005688934138618034243, 0.007580434474681629550 ),
 .UNSPECIFIED. ) ;
#9882=CARTESIAN_POINT ( 'NONE',  ( 0.000000000000000000, 0.000000000000000000, 19.04999999999996874 ) ) ;
#9885=( LENGTH_UNIT ( ) NAMED_UNIT ( * ) SI_UNIT ( .MILLI., .METRE. ) );
#9886=CARTESIAN_POINT ( 'NONE',  ( 1.432654583217642275, -3.458734124999999437, 2.050000001365597679 ) ) ;
#9887=CARTESIAN_POINT ( 'NONE',  ( -3.458734125000000326, 0.000000000000000000, 1.737500001365596347 ) ) ;
#9890=SURFACE_SIDE_STYLE ('',( #989 ) ) ;
#9891=CARTESIAN_POINT ( 'NONE',  ( -4.000000000000000000, 4.898587196589412829E-16, 19.04999999999996874 ) ) ;
#9894=AXIS2_PLACEMENT_3D ( 'NONE', #18206, #12370, #17971 ) ;
#9896=CARTESIAN_POINT ( 'NONE',  ( 1.432654583217640276, 3.458734125000000770, -2.324999998634404097 ) ) ;
#9898=STYLED_ITEM ( 'NONE', ( #4355 ), #6915 ) ;
#9900=( GEOMETRIC_REPRESENTATION_CONTEXT ( 3 ) GLOBAL_UNCERTAINTY_ASSIGNED_CONTEXT ( ( #15324 ) ) GLOBAL_UNIT_ASSIGNED_CONTEXT ( ( #9885, #7490, #17058 ) ) REPRESENTATION_CONTEXT ( 'NONE', 'WORKASPACE' ) );
#9906=CARTESIAN_POINT ( 'NONE',  ( 1.432654583217640276, 3.458734125000000770, 5.675000001365596347 ) ) ;
#9914=CARTESIAN_POINT ( 'NONE',  ( -1.656854249492380804, 4.000000000000000000, 5.237500002731186655 ) ) ;
#9920=AXIS2_PLACEMENT_3D ( 'NONE', #16272, #23682, #12704 ) ;
#9924=VECTOR ( 'NONE', #9365, 1000.000000000000000 ) ;
#9933=CARTESIAN_POINT ( 'NONE',  ( -1.067197363239236862, -6.889406814520513400, -3.442664554191213977 ) ) ;
#9940=CARTESIAN_POINT ( 'NONE',  ( 3.999999999999999112, 1.505528603326912629, 1.981791683554507300 ) ) ;
#9942=AXIS2_PLACEMENT_3D ( 'NONE', #18909, #11399, #18552 ) ;
#9973=CARTESIAN_POINT ( 'NONE',  ( -4.000000000000000000, 0.000000000000000000, 2.300000000000001599 ) ) ;
#10001=CARTESIAN_POINT ( 'NONE',  ( -2.445694354108820523, 2.445694354108820523, 1.862500001365596347 ) ) ;
#10005=ADVANCED_FACE ( 'NONE', ( #18361 ), #12995, .T. ) ;
#10013=CARTESIAN_POINT ( 'NONE',  ( 3.458734125000000326, 4.235727675282971730E-16, 0.2375000013655967357 ) ) ;
#10014=CARTESIAN_POINT ( 'NONE',  ( -1.432654583217640942, -3.458734124999999882, 0.9250000013655965692 ) ) ;
#10017=( NAMED_UNIT ( * ) PLANE_ANGLE_UNIT ( ) SI_UNIT ( $, .RADIAN. ) );
#10018=ORIENTED_EDGE ( 'NONE', *, *, #12301, .F. ) ;
#10023=CARTESIAN_POINT ( 'NONE',  ( -3.458734125000000326, -1.432654583217642497, -2.949999998634404985 ) ) ;
#10032=CARTESIAN_POINT ( 'NONE',  ( 1.432654583217642275, -3.458734124999999882, 5.300000001365596347 ) ) ;
#10071=CARTESIAN_POINT ( 'NONE',  ( 5.434916218090827478, 4.367703157927330437, -3.442152416367929568 ) ) ;
#10088=CARTESIAN_POINT ( 'NONE',  ( -4.000000000000000000, -1.656854249492383246, -0.6374999999999969580 ) ) ;
#10104=CARTESIAN_POINT ( 'NONE',  ( -2.828427124746190291, 2.828427124746190291, -0.6999999972688124572 ) ) ;
#10108=EDGE_CURVE ( 'NONE', #19663, #10566, #461, .T. ) ;
#10113=CARTESIAN_POINT ( 'NONE',  ( 3.458734125000000770, 4.235727675282972223E-16, 3.487500001365597679 ) ) ;
#10122=CARTESIAN_POINT ( 'NONE',  ( -3.458734125000000326, 1.432654583217640276, 0.6750000013655963471 ) ) ;
#10124=CARTESIAN_POINT ( 'NONE',  ( -1.432654583217640276, 3.458734125000000326, -0.4499999986344046521 ) ) ;
#10127=( LENGTH_UNIT ( ) NAMED_UNIT ( * ) SI_UNIT ( .MILLI., .METRE. ) );
#10129=VERTEX_POINT ( 'NONE', #4337 ) ;
#10136=CARTESIAN_POINT ( 'NONE',  ( -1.432654583217640498, 3.458734125000000770, -3.199999998634403209 ) ) ;
#10146=CARTESIAN_POINT ( 'NONE',  ( 1.432654583217642275, -3.458734124999999882, 1.300000001365597235 ) ) ;
#10156=CARTESIAN_POINT ( 'NONE',  ( 4.000000000000000000, 1.656854249492381248, 2.987500002731188431 ) ) ;
#10158=VERTEX_POINT ( 'NONE', #4693 ) ;
#10167=VECTOR ( 'NONE', #5502, 1000.000000000000000 ) ;
#10199=ORIENTED_EDGE ( 'NONE', *, *, #12946, .F. ) ;
#10209=CARTESIAN_POINT ( 'NONE',  ( 7.347880794884118750E-16, -4.000000000000000000, -2.449999999999998845 ) ) ;
#10222=CARTESIAN_POINT ( 'NONE',  ( 1.656854249492380138, 4.000000000000000000, -0.8874999972688127903 ) ) ;
#10227=CARTESIAN_POINT ( 'NONE',  ( 6.500000000000000000, -3.142418015001833265, -0.4043611937012248636 ) ) ;
#10231=CIRCLE ( 'NONE', #2548, 6.500000000000000888 ) ;
#10232=CARTESIAN_POINT ( 'NONE',  ( -3.458734125000000770, 1.432654583217640498, -1.074999998634403209 ) ) ;
#10243=CARTESIAN_POINT ( 'NONE',  ( -1.432654583217640276, 3.458734125000000326, 0.5500000013655963471 ) ) ;
#10253=AXIS2_PLACEMENT_3D ( 'NONE', #1499, #16246, #19936 ) ;
#10265=CARTESIAN_POINT ( 'NONE',  ( -2.117863837641485618E-16, 3.458734125000000770, 2.737500001365597235 ) ) ;
#10271=CARTESIAN_POINT ( 'NONE',  ( 2.828427124746189847, 2.828427124746190291, -2.074999999999998845 ) ) ;
#10274=CARTESIAN_POINT ( 'NONE',  ( 2.828427124746190735, -2.828427124746189847, 0.8000000027311872097 ) ) ;
#10282=ORIENTED_EDGE ( 'NONE', *, *, #3538, .F. ) ;
#10294=CARTESIAN_POINT ( 'NONE',  ( 2.445694354108820523, -2.445694354108820079, 3.112500001365597679 ) ) ;
#10300=ORIENTED_EDGE ( 'NONE', *, *, #6631, .F. ) ;
#10313=CIRCLE ( 'NONE', #10702, 6.500000000000000888 ) ;
#10316=CARTESIAN_POINT ( 'NONE',  ( 0.000000000000000000, 0.000000000000000000, 3.059999999999998277 ) ) ;
#10335=CARTESIAN_POINT ( 'NONE',  ( -2.117863837641485618E-16, 3.458734125000000326, -1.512499998634402987 ) ) ;
#10355=CARTESIAN_POINT ( 'NONE',  ( -3.458734125000000770, 0.000000000000000000, 0.9875000013655956810 ) ) ;
#10356=CARTESIAN_POINT ( 'NONE',  ( 0.000000000000000000, 0.000000000000000000, 19.04999999999996874 ) ) ;
#10359=DIRECTION ( 'NONE',  ( 0.000000000000000000, 0.000000000000000000, -1.000000000000000000 ) ) ;
#10376=ADVANCED_FACE ( 'NONE', ( #16080 ), #16193, .T. ) ;
#10379=CARTESIAN_POINT ( 'NONE',  ( -3.251184232703611343, 2.330193357860981251, -3.674599999999999866 ) ) ;
#10390=CARTESIAN_POINT ( 'NONE',  ( 1.432654583217640276, 3.458734125000000770, 0.6750000013655963471 ) ) ;
#10399=CARTESIAN_POINT ( 'NONE',  ( 4.000000000000000888, -1.656854249492379694, -1.137499997268811125 ) ) ;
#10413=DIRECTION ( 'NONE',  ( -0.000000000000000000, 0.000000000000000000, -1.000000000000000000 ) ) ;
#10417=CARTESIAN_POINT ( 'NONE',  ( -1.432654583217640942, -3.458734124999999882, 4.925000001365594571 ) ) ;
#10422=CARTESIAN_POINT ( 'NONE',  ( -3.265986985212536720, 1.709698821660321499, 2.039999999999996927 ) ) ;
#10431=CYLINDRICAL_SURFACE ( 'NONE', #5684, 4.714285714285714413 ) ;
#10442=CARTESIAN_POINT ( 'NONE',  ( 4.000000000000000000, 0.000000000000000000, 19.04999999999996874 ) ) ;
#10447=CARTESIAN_POINT ( 'NONE',  ( -6.500000000000000000, -3.142418015001830600, -3.295638806298776036 ) ) ;
#10449=CARTESIAN_POINT ( 'NONE',  ( 2.828427124746190735, -2.828427124746189847, -1.324999999999997957 ) ) ;
#10471=CARTESIAN_POINT ( 'NONE',  ( 3.458734125000000770, 1.432654583217640498, -1.449999998634403653 ) ) ;
#10489=VERTEX_POINT ( 'NONE', #10934 ) ;
#10501=CARTESIAN_POINT ( 'NONE',  ( -1.432654583217641164, -3.458734125000000326, 2.175000001365597679 ) ) ;
#10502=CARTESIAN_POINT ( 'NONE',  ( 1.125461230421587633, -3.270501301980698550, 2.040000000000001812 ) ) ;
#10510=CARTESIAN_POINT ( 'NONE',  ( -2.828427124746190291, 2.828427124746190291, -1.699999997268811569 ) ) ;
#10530=CARTESIAN_POINT ( 'NONE',  ( -2.117863837641485618E-16, 3.458734125000000326, 3.487500001365594571 ) ) ;
#10533=EDGE_CURVE ( 'NONE', #12546, #15256, #12967, .T. ) ;
#10543=EDGE_CURVE ( 'NONE', #10566, #21201, #13378, .T. ) ;
#10551=AXIS2_PLACEMENT_3D ( 'NONE', #13672, #4551, #11888 ) ;
#10555=CARTESIAN_POINT ( 'NONE',  ( 4.000000000000000000, 4.898587196589412829E-16, -0.1999999999999987899 ) ) ;
#10558=EDGE_CURVE ( 'NONE', #2314, #3785, #11565, .T. ) ;
#10566=VERTEX_POINT ( 'NONE', #5634 ) ;
#10567=CARTESIAN_POINT ( 'NONE',  ( -2.828427124746190291, 2.828427124746190291, -2.824999999999997513 ) ) ;
#10571=CARTESIAN_POINT ( 'NONE',  ( 6.500000000000000000, -3.752776749732574135, -3.700000000000000178 ) ) ;
#10575=CARTESIAN_POINT ( 'NONE',  ( -1.432654583217640276, 3.458734125000000326, -2.449999998634404097 ) ) ;
#10587=CONICAL_SURFACE ( 'NONE', #10951, 6.500000000000000888, 1.047197551196596521 ) ;
#10593=CARTESIAN_POINT ( 'NONE',  ( 3.458734125000000770, 4.235727675282972223E-16, -0.5124999986344038749 ) ) ;
#10622=CARTESIAN_POINT ( 'NONE',  ( -3.458734125000000770, 0.000000000000000000, -0.01249999863440348635 ) ) ;
#10628=ORIENTED_EDGE ( 'NONE', *, *, #23560, .T. ) ;
#10630=CARTESIAN_POINT ( 'NONE',  ( 4.000000000000000000, 1.656854249492381248, 1.987500002731187765 ) ) ;
#10634=VERTEX_POINT ( 'NONE', #3707 ) ;
#10642=CONICAL_SURFACE ( 'NONE', #20156, 6.500000000000000888, 1.047197551196596521 ) ;
#10648=CARTESIAN_POINT ( 'NONE',  ( -1.432654583217640942, -3.458734124999999882, 2.925000001365598123 ) ) ;
#10656=( BOUNDED_CURVE ( )  B_SPLINE_CURVE ( 2, ( #15667, #2573, #661, #898, #21127, #4499, #22815, #13745, #9793 ),
 .UNSPECIFIED., .F., .F. ) 
 B_SPLINE_CURVE_WITH_KNOTS ( ( 3, 2, 2, 2, 3 ),
 ( 0.3499999999999999778, 0.3624999999999999889, 0.3750000000000000000, 0.3875000000000000111, 0.4000000000000000222 ),
 .UNSPECIFIED. ) 
 CURVE ( )  GEOMETRIC_REPRESENTATION_ITEM ( )  RATIONAL_B_SPLINE_CURVE ( ( 1.000000000000000000, 0.9238795325112867385, 1.000000000000000000, 0.9238795325112867385, 1.000000000000000000, 0.9238795325112867385, 1.000000000000000000, 0.9238795325112867385, 1.000000000000000000 ) ) 
 REPRESENTATION_ITEM ( '' )  );
#10683=FACE_OUTER_BOUND ( 'NONE', #12838, .T. ) ;
#10686=DIRECTION ( 'NONE',  ( 0.000000000000000000, 0.000000000000000000, 1.000000000000000000 ) ) ;
#10690=CARTESIAN_POINT ( 'NONE',  ( 3.458734125000000326, 4.235727675282971730E-16, -1.762499998634403209 ) ) ;
#10702=AXIS2_PLACEMENT_3D ( 'NONE', #17546, #8925, #14074 ) ;
#10704=B_SPLINE_CURVE_WITH_KNOTS ( 'NONE', 3,
 ( #20571, #6220, #13782, #4178, #11986, #11871 ),
 .UNSPECIFIED., .F., .F.,
 ( 4, 2, 4 ),
 ( 2.380733003126162433E-07, 0.001898835937927379836, 0.003797433802554446743 ),
 .UNSPECIFIED. ) ;
#10706=ADVANCED_FACE ( 'NONE', ( #7917 ), #11536, .F. ) ;
#10710=CARTESIAN_POINT ( 'NONE',  ( -3.458734125000000770, 1.432654583217640498, -0.07499999863440427739 ) ) ;
#10723=ORIENTED_EDGE ( 'NONE', *, *, #10956, .T. ) ;
#10724=CARTESIAN_POINT ( 'NONE',  ( -4.000000000000000000, 0.000000000000000000, -2.699999999999999289 ) ) ;
#10725=AXIS2_PLACEMENT_3D ( 'NONE', #23337, #6946, #19852 ) ;
#10749=ORIENTED_EDGE ( 'NONE', *, *, #18837, .F. ) ;
#10753=CARTESIAN_POINT ( 'NONE',  ( 7.347880794884118750E-16, -4.000000000000000000, -0.3249999972688121241 ) ) ;
#10767=LINE ( 'NONE', #18042, #7053 ) ;
#10771=CARTESIAN_POINT ( 'NONE',  ( -1.432654583217640276, 3.458734125000000326, 1.550000001365597013 ) ) ;
#10777=CARTESIAN_POINT ( 'NONE',  ( -3.544972969423974440, -0.09312760838339886882, 2.039999999999999591 ) ) ;
#10786=VERTEX_POINT ( 'NONE', #3459 ) ;
#10802=CARTESIAN_POINT ( 'NONE',  ( 6.500000000000000000, 3.752776749732563477, -3.700000000000000178 ) ) ;
#10810=CARTESIAN_POINT ( 'NONE',  ( -3.458734124999999882, -1.432654583217642497, -2.199999998634404541 ) ) ;
#10825=CARTESIAN_POINT ( 'NONE',  ( 4.000000000000000000, 1.656854249492381248, 5.862500000000002487 ) ) ;
#10826=CARTESIAN_POINT ( 'NONE',  ( 2.828427124746190735, -2.828427124746189847, 0.6750000000000020428 ) ) ;
#10830=ORIENTED_EDGE ( 'NONE', *, *, #16060, .T. ) ;
#10838=CARTESIAN_POINT ( 'NONE',  ( -2.117863837641485618E-16, 3.458734125000000326, -1.512499998634402987 ) ) ;
#10859=CARTESIAN_POINT ( 'NONE',  ( 3.458734125000000326, 1.432654583217640498, 5.300000001365596347 ) ) ;
#10867=ORIENTED_EDGE ( 'NONE', *, *, #19706, .T. ) ;
#10875=CARTESIAN_POINT ( 'NONE',  ( -1.065083781909173410, 6.890627091270371096, -3.442152416367929124 ) ) ;
#10878=CARTESIAN_POINT ( 'NONE',  ( -2.445694354108820523, 2.445694354108820523, -1.387499998634402987 ) ) ;
#10902=B_SPLINE_CURVE_WITH_KNOTS ( 'NONE', 3,
 ( #8010, #2588, #9933, #11508, #18780, #21023 ),
 .UNSPECIFIED., .F., .F.,
 ( 4, 2, 4 ),
 ( 2.380733003329415929E-07, 0.001898835937927393280, 0.003797433802554453681 ),
 .UNSPECIFIED. ) ;
#10906=CARTESIAN_POINT ( 'NONE',  ( -2.117863837641483646E-16, 3.458734125000000770, -3.295601554149324208 ) ) ;
#10924=VERTEX_POINT ( 'NONE', #14382 ) ;
#10934=CARTESIAN_POINT ( 'NONE',  ( -1.647987302177966740E-14, -7.505553499465137612, -0.5805565836007695601 ) ) ;
#10937=CARTESIAN_POINT ( 'NONE',  ( 1.656854249492383024, -3.999999999999999112, 3.612500000000005596 ) ) ;
#10951=AXIS2_PLACEMENT_3D ( 'NONE', #13644, #8251, #15570 ) ;
#10956=EDGE_CURVE ( 'NONE', #15043, #6042, #4187, .T. ) ;
#10963=FACE_OUTER_BOUND ( 'NONE', #42, .T. ) ;
#10972=CARTESIAN_POINT ( 'NONE',  ( 1.656854249492383024, -3.999999999999999112, -3.262499997268812901 ) ) ;
#10981=CARTESIAN_POINT ( 'NONE',  ( -2.445694354108819635, -2.445694354108820967, 0.1125000013655966247 ) ) ;
#10988=CARTESIAN_POINT ( 'NONE',  ( 3.458734125000000326, 1.432654583217640498, -1.699999998634404097 ) ) ;
#10991=EDGE_CURVE ( 'NONE', #15816, #19016, #2306, .T. ) ;
#10995=CARTESIAN_POINT ( 'NONE',  ( 6.500000000000000000, -0.6341575537611440216, -3.700000000000001066 ) ) ;
#10998=ORIENTED_EDGE ( 'NONE', *, *, #15009, .T. ) ;
#11032=CARTESIAN_POINT ( 'NONE',  ( 3.458734125000000770, -1.432654583217639610, -0.8249999986344030978 ) ) ;
#11034=ORIENTED_EDGE ( 'NONE', *, *, #20606, .T. ) ;
#11043=PLANE ( 'NONE',  #12999 ) ;
#11053=CARTESIAN_POINT ( 'NONE',  ( -1.432654583217641164, -3.458734125000000326, -2.824999998634404985 ) ) ;
#11057=ORIENTED_EDGE ( 'NONE', *, *, #11465, .T. ) ;
#11058=CIRCLE ( 'NONE', #15271, 6.500000000000000888 ) ;
#11077=CARTESIAN_POINT ( 'NONE',  ( 0.000000000000000000, 0.000000000000000000, 2.039999999999998259 ) ) ;
#11089=CARTESIAN_POINT ( 'NONE',  ( -3.458734125000000326, 1.432654583217640276, 4.675000001365594571 ) ) ;
#11091=ORIENTED_EDGE ( 'NONE', *, *, #3345, .T. ) ;
#11094=EDGE_CURVE ( 'NONE', #9522, #8785, #21125, .T. ) ;
#11098=CARTESIAN_POINT ( 'NONE',  ( -4.000000000000000000, 0.000000000000000000, -2.574999997268812457 ) ) ;
#11103=CARTESIAN_POINT ( 'NONE',  ( -3.458734125000000770, 1.432654583217640498, -1.074999998634403431 ) ) ;
#11111=CARTESIAN_POINT ( 'NONE',  ( 1.432654583217639832, 3.458734125000000326, 0.4250000013655961251 ) ) ;
#11131=AXIS2_PLACEMENT_3D ( 'NONE', #2875, #2649, #8423 ) ;
#11134=EDGE_CURVE ( 'NONE', #10129, #8578, #19432, .T. ) ;
#11163=DIRECTION ( 'NONE',  ( 1.000000000000000000, 0.000000000000000000, 0.000000000000000000 ) ) ;
#11179=CARTESIAN_POINT ( 'NONE',  ( 4.000000000000000000, 4.898587196589412829E-16, 5.800000000000001599 ) ) ;
#11210=CARTESIAN_POINT ( 'NONE',  ( 2.828427124746189847, 2.828427124746190291, -2.949999997268812901 ) ) ;
#11219=CARTESIAN_POINT ( 'NONE',  ( 1.432654583217640276, 3.458734125000000770, -0.3249999986344045411 ) ) ;
#11222=LINE ( 'NONE', #4008, #7802 ) ;
#11224=LINE ( 'NONE', #18498, #15323 ) ;
#11226=CARTESIAN_POINT ( 'NONE',  ( -3.458734125000000326, 0.000000000000000000, -1.262499998634402765 ) ) ;
#11239=ORIENTED_EDGE ( 'NONE', *, *, #6871, .F. ) ;
#11241=ORIENTED_EDGE ( 'NONE', *, *, #137, .T. ) ;
#11259=CARTESIAN_POINT ( 'NONE',  ( -3.250000000000004441, 5.629165124598849879, 0.000000000000000000 ) ) ;
#11264=EDGE_CURVE ( 'NONE', #8578, #6397, #10902, .T. ) ;
#11286=CARTESIAN_POINT ( 'NONE',  ( 7.347880794884118750E-16, -4.000000000000000000, -0.3249999972688121241 ) ) ;
#11290=CARTESIAN_POINT ( 'NONE',  ( -3.458734125000000770, 0.000000000000000000, -3.012499998634404541 ) ) ;
#11291=CARTESIAN_POINT ( 'NONE',  ( -1.656854249492381248, -3.999999999999999112, 5.487500000000000711 ) ) ;
#11297=ADVANCED_FACE ( 'NONE', ( #6677 ), #19005, .F. ) ;
#11298=VERTEX_POINT ( 'NONE', #3518 ) ;
#11304=ORIENTED_EDGE ( 'NONE', *, *, #21192, .T. ) ;
#11334=CARTESIAN_POINT ( 'NONE',  ( 1.432654583217639832, 3.458734125000000326, 4.425000001365595459 ) ) ;
#11343=CIRCLE ( 'NONE', #1744, 6.500000000000000888 ) ;
#11345=CARTESIAN_POINT ( 'NONE',  ( -3.458734125000000770, 1.432654583217640498, 1.925000001365597457 ) ) ;
#11350=CARTESIAN_POINT ( 'NONE',  ( 3.458734125000000770, -1.432654583217639610, -2.824999998634404985 ) ) ;
#11372=CARTESIAN_POINT ( 'NONE',  ( -4.000000000000000000, 0.000000000000000000, 0.4250000027311868211 ) ) ;
#11374=CARTESIAN_POINT ( 'NONE',  ( 3.007318562400188799, 2.637429632093199139, 2.039999999999998259 ) ) ;
#11378=CARTESIAN_POINT ( 'NONE',  ( -1.065083781909173410, 6.890627091270371096, -0.2578475836320718306 ) ) ;
#11387=CARTESIAN_POINT ( 'NONE',  ( -1.301042606982605321E-15, 7.505553499465137612, -3.119443416399232394 ) ) ;
#11399=DIRECTION ( 'NONE',  ( -0.000000000000000000, -0.000000000000000000, 1.000000000000000000 ) ) ;
#11414=CARTESIAN_POINT ( 'NONE',  ( -2.828427124746190291, 2.828427124746190291, 2.175000000000001599 ) ) ;
#11418=ORIENTED_EDGE ( 'NONE', *, *, #2604, .T. ) ;
#11437=EDGE_CURVE ( 'NONE', #844, #15758, #3856, .T. ) ;
#11445=CARTESIAN_POINT ( 'NONE',  ( 2.445694354108820079, 2.445694354108820523, 5.612500001365596347 ) ) ;
#11453=CARTESIAN_POINT ( 'NONE',  ( -2.445694354108820523, 2.445694354108820523, 3.612500001365594571 ) ) ;
#11455=CARTESIAN_POINT ( 'NONE',  ( 4.000000000000000000, 1.656854249492381248, 1.862500000000001599 ) ) ;
#11465=EDGE_CURVE ( 'NONE', #10566, #6989, #20281, .T. ) ;
#11466=CARTESIAN_POINT ( 'NONE',  ( -1.432654583217641164, -3.458734125000000326, -0.8249999986344029868 ) ) ;
#11472=VECTOR ( 'NONE', #19502, 1000.000000000000000 ) ;
#11475=CARTESIAN_POINT ( 'NONE',  ( 2.445694354108820523, -2.445694354108820079, -2.887499998634404097 ) ) ;
#11487=EDGE_LOOP ( 'NONE', ( #3318, #3813, #18171 ) ) ;
#11502=VECTOR ( 'NONE', #13858, 1000.000000000000000 ) ;
#11506=FACE_OUTER_BOUND ( 'NONE', #22638, .T. ) ;
#11508=CARTESIAN_POINT ( 'NONE',  ( -2.149474931388143606, -6.264553569211847694, -3.644669744206375572 ) ) ;
#11531=FACE_OUTER_BOUND ( 'NONE', #20333, .T. ) ;
#11536=CYLINDRICAL_SURFACE ( 'NONE', #5317, 4.000000000000000000 ) ;
#11541=CARTESIAN_POINT ( 'NONE',  ( -1.432654583217640498, 3.458734125000000770, -2.199999998634404541 ) ) ;
#11542=CARTESIAN_POINT ( 'NONE',  ( 2.828427124746189847, 2.828427124746190291, -0.07499999999999867883 ) ) ;
#11565=( BOUNDED_CURVE ( )  B_SPLINE_CURVE ( 2, ( #16543, #1793, #14764, #7565, #11286, #7342, #12741, #16657, #22018 ),
 .UNSPECIFIED., .F., .F. ) 
 B_SPLINE_CURVE_WITH_KNOTS ( ( 3, 2, 2, 2, 3 ),
 ( 0.5500000000000000444, 0.5625000000000000000, 0.5749999999999999556, 0.5875000000000000222, 0.5999999999999999778 ),
 .UNSPECIFIED. ) 
 CURVE ( )  GEOMETRIC_REPRESENTATION_ITEM ( )  RATIONAL_B_SPLINE_CURVE ( ( 1.000000000000000000, 0.9238795325112867385, 1.000000000000000000, 0.9238795325112867385, 1.000000000000000000, 0.9238795325112867385, 1.000000000000000000, 0.9238795325112867385, 1.000000000000000000 ) ) 
 REPRESENTATION_ITEM ( '' )  );
#11566=CARTESIAN_POINT ( 'NONE',  ( 1.432654583217642275, -3.458734124999999882, 4.300000001365595459 ) ) ;
#11575=CARTESIAN_POINT ( 'NONE',  ( 1.432654583217642275, -3.458734124999999437, 3.050000001365598568 ) ) ;
#11576=ADVANCED_FACE ( 'NONE', ( #21056 ), #6557, .T. ) ;
#11584=CARTESIAN_POINT ( 'NONE',  ( 2.445694354108820967, -2.445694354108820079, -1.637499998634403209 ) ) ;
#11588=ADVANCED_FACE ( 'NONE', ( #16054 ), #19971, .T. ) ;
#11593=CARTESIAN_POINT ( 'NONE',  ( -2.445694354108820523, 2.445694354108820523, -3.387499998634403209 ) ) ;
#11598=CARTESIAN_POINT ( 'NONE',  ( -5.479999999999998650, 7.335634326892644012E-16, 3.059999999999998277 ) ) ;
#11601=CARTESIAN_POINT ( 'NONE',  ( -4.000000000000000000, 0.000000000000000000, 5.425000002731187543 ) ) ;
#11612=ORIENTED_EDGE ( 'NONE', *, *, #20402, .F. ) ;
#11637=CARTESIAN_POINT ( 'NONE',  ( -1.656854249492380582, 4.000000000000000000, 1.112500000000000711 ) ) ;
#11642=APPLICATION_CONTEXT ( 'automotive_design' ) ;
#11645=DIRECTION ( 'NONE',  ( 0.000000000000000000, 0.000000000000000000, -1.000000000000000000 ) ) ;
#11653=CARTESIAN_POINT ( 'NONE',  ( 6.500000000000001776, 0.6345343291280539644, 5.336307567702092136E-16 ) ) ;
#11654=ORIENTED_EDGE ( 'NONE', *, *, #7527, .F. ) ;
#11655=CARTESIAN_POINT ( 'NONE',  ( -1.656854249492381248, -3.999999999999999112, -0.5124999999999969580 ) ) ;
#11668=ORIENTED_EDGE ( 'NONE', *, *, #21650, .F. ) ;
#11679=CARTESIAN_POINT ( 'NONE',  ( -2.445694354108820523, 2.445694354108820523, 4.862500001365595459 ) ) ;
#11688=CARTESIAN_POINT ( 'NONE',  ( -1.432654583217640942, -3.458734124999999882, 2.925000001365598123 ) ) ;
#11689=CARTESIAN_POINT ( 'NONE',  ( -1.432654583217640942, -3.458734124999999882, -0.07499999863440427739 ) ) ;
#11698=CARTESIAN_POINT ( 'NONE',  ( 3.458734125000000770, 4.235727675282972223E-16, -2.512499998634404097 ) ) ;
#11708=CARTESIAN_POINT ( 'NONE',  ( -3.458734124999999882, -1.432654583217642497, -2.199999998634404541 ) ) ;
#11716=CARTESIAN_POINT ( 'NONE',  ( 1.656854249492383024, -3.999999999999999112, 4.737500002731186655 ) ) ;
#11725=EDGE_CURVE ( 'NONE', #8139, #21232, #23430, .T. ) ;
#11754=EDGE_CURVE ( 'NONE', #7010, #13210, #2245, .T. ) ;
#11760=EDGE_CURVE ( 'NONE', #14122, #10129, #7718, .T. ) ;
#11761=VERTEX_POINT ( 'NONE', #14623 ) ;
#11770=CARTESIAN_POINT ( 'NONE',  ( 4.000000000000000000, 4.898587196589412829E-16, 2.800000000000002043 ) ) ;
#11790=EDGE_CURVE ( 'NONE', #669, #4306, #1957, .T. ) ;
#11797=CARTESIAN_POINT ( 'NONE',  ( -2.445694354108819635, -2.445694354108820967, 2.112500001365596791 ) ) ;
#11807=CARTESIAN_POINT ( 'NONE',  ( -3.458734124999999882, -1.432654583217642497, 2.800000001365598123 ) ) ;
#11808=CARTESIAN_POINT ( 'NONE',  ( -1.432654583217640942, -3.458734124999999882, -1.074999998634403431 ) ) ;
#11817=CARTESIAN_POINT ( 'NONE',  ( -3.802871176606132497, -5.309964801958124703, -3.686277791023380601 ) ) ;
#11825=CARTESIAN_POINT ( 'NONE',  ( 2.445694354108820967, -2.445694354108820079, 5.362500001365596347 ) ) ;
#11835=CARTESIAN_POINT ( 'NONE',  ( -4.000000000000000000, 0.000000000000000000, 3.425000002731189319 ) ) ;
#11871=CARTESIAN_POINT ( 'NONE',  ( 3.250000000000003109, 5.629165124598848102, 1.734723475976807094E-15 ) ) ;
#11878=CARTESIAN_POINT ( 'NONE',  ( 6.499999999999999112, 2.531211054341943711, -3.440493080744402299 ) ) ;
#11879=CARTESIAN_POINT ( 'NONE',  ( -4.000000000000000000, 4.898587196589412829E-16, 19.04999999999996874 ) ) ;
#11882=CIRCLE ( 'NONE', #16837, 6.499999999999999112 ) ;
#11888=DIRECTION ( 'NONE',  ( 1.000000000000000000, 0.000000000000000000, 0.000000000000000000 ) ) ;
#11892=CARTESIAN_POINT ( 'NONE',  ( 7.347880794884118750E-16, -4.000000000000000000, 2.550000000000002043 ) ) ;
#11897=ORIENTED_EDGE ( 'NONE', *, *, #1743, .T. ) ;
#11906=VERTEX_POINT ( 'NONE', #16994 ) ;
#11908=CARTESIAN_POINT ( 'NONE',  ( -4.000000000000000000, 0.000000000000000000, -0.5749999972688123462 ) ) ;
#11919=CARTESIAN_POINT ( 'NONE',  ( -1.432654583217641164, -3.458734125000000326, 5.175000001365595459 ) ) ;
#11923=AXIS2_PLACEMENT_3D ( 'NONE', #8051, #8402, #19159 ) ;
#11930=CARTESIAN_POINT ( 'NONE',  ( 1.432654583217639832, 3.458734125000000326, 2.425000001365597679 ) ) ;
#11932=CARTESIAN_POINT ( 'NONE',  ( -2.445694354108820523, 2.445694354108820523, -0.3874999986344038194 ) ) ;
#11936=FILL_AREA_STYLE_COLOUR ( '', #16010 ) ;
#11942=CARTESIAN_POINT ( 'NONE',  ( 6.353591512924457348E-16, -3.458734125000000770, -2.762499998634404097 ) ) ;
#11950=CARTESIAN_POINT ( 'NONE',  ( 3.458734125000000770, 4.235727675282972223E-16, 0.4875000013655969577 ) ) ;
#11958=CARTESIAN_POINT ( 'NONE',  ( -1.656854249492380804, 4.000000000000000000, 3.237500002731188875 ) ) ;
#11960=ORIENTED_EDGE ( 'NONE', *, *, #21194, .T. ) ;
#11965=UNCERTAINTY_MEASURE_WITH_UNIT (LENGTH_MEASURE( 1.000000000000000082E-05 ), #10127, 'distance_accuracy_value', 'NONE');
#11986=CARTESIAN_POINT ( 'NONE',  ( 2.696295709017752618, 5.948846446048902337, 4.712891318522927087E-15 ) ) ;
#11996=LINE ( 'NONE', #10442, #11472 ) ;
#12004=CARTESIAN_POINT ( 'NONE',  ( 4.000000000000000000, 1.656854249492381248, -2.137499999999997957 ) ) ;
#12007=LINE ( 'NONE', #19272, #3560 ) ;
#12013=ORIENTED_EDGE ( 'NONE', *, *, #10533, .F. ) ;
#12022=VECTOR ( 'NONE', #19384, 1000.000000000000000 ) ;
#12031=CARTESIAN_POINT ( 'NONE',  ( 3.458734125000000770, 1.432654583217640498, 0.5500000013655963471 ) ) ;
#12032=CYLINDRICAL_SURFACE ( 'NONE', #3028, 4.000000000000000000 ) ;
#12040=CARTESIAN_POINT ( 'NONE',  ( 3.458734125000001214, -1.432654583217639610, 0.1750000013655959863 ) ) ;
#12046=PRODUCT ( 'torque nut 08a_iso_ISO 10511-M8-N', 'torque nut 08a_iso_ISO 10511-M8-N', '', ( #13215 ) ) ;
#12051=CARTESIAN_POINT ( 'NONE',  ( -2.445694354108819635, -2.445694354108820967, -2.887499998634404097 ) ) ;
#12060=CARTESIAN_POINT ( 'NONE',  ( 1.432654583217642275, -3.458734124999999882, 2.300000001365597679 ) ) ;
#12067=ORIENTED_EDGE ( 'NONE', *, *, #8201, .T. ) ;
#12071=CARTESIAN_POINT ( 'NONE',  ( 2.828427124746190735, -2.828427124746189847, 4.800000002731187543 ) ) ;
#12087=CARTESIAN_POINT ( 'NONE',  ( 1.432654583217639832, 3.458734125000000326, 5.425000001365595459 ) ) ;
#12100=LINE ( 'NONE', #12578, #6030 ) ;
#12108=CARTESIAN_POINT ( 'NONE',  ( -3.250000000000004441, 5.629165124598849879, 0.000000000000000000 ) ) ;
#12113=CARTESIAN_POINT ( 'NONE',  ( 4.000000000000000888, -1.656854249492379694, -1.137499997268811125 ) ) ;
#12119=CARTESIAN_POINT ( 'NONE',  ( -1.656854249492380804, 4.000000000000000000, -2.887499999999997513 ) ) ;
#12125=DIRECTION ( 'NONE',  ( 6.123233995736827666E-17, -1.000000000000000000, 0.000000000000000000 ) ) ;
#12134=CARTESIAN_POINT ( 'NONE',  ( 2.828427124746189847, 2.828427124746190291, -0.9499999972688126793 ) ) ;
#12141=CARTESIAN_POINT ( 'NONE',  ( -1.432654583217641164, -3.458734125000000326, -1.824999998634404097 ) ) ;
#12155=DIRECTION ( 'NONE',  ( 0.000000000000000000, 0.000000000000000000, -1.000000000000000000 ) ) ;
#12156=ORIENTED_EDGE ( 'NONE', *, *, #15990, .T. ) ;
#12174=CARTESIAN_POINT ( 'NONE',  ( 3.458734125000000770, 4.235727675282972223E-16, 3.487500001365597679 ) ) ;
#12184=CARTESIAN_POINT ( 'NONE',  ( -1.656854249492380804, 4.000000000000000000, 0.2375000027311863493 ) ) ;
#12190=( BOUNDED_CURVE ( )  B_SPLINE_CURVE ( 2, ( #11372, #16744, #324, #9579, #203, #13058, #5840, #22467, #9806 ),
 .UNSPECIFIED., .F., .F. ) 
 B_SPLINE_CURVE_WITH_KNOTS ( ( 3, 2, 2, 2, 3 ),
 ( 0.5000000000000000000, 0.5124999999999999556, 0.5250000000000000222, 0.5374999999999999778, 0.5500000000000000444 ),
 .UNSPECIFIED. ) 
 CURVE ( )  GEOMETRIC_REPRESENTATION_ITEM ( )  RATIONAL_B_SPLINE_CURVE ( ( 1.000000000000000000, 0.9238795325112867385, 1.000000000000000000, 0.9238795325112867385, 1.000000000000000000, 0.9238795325112867385, 1.000000000000000000, 0.9238795325112867385, 1.000000000000000000 ) ) 
 REPRESENTATION_ITEM ( '' )  );
#12192=ORIENTED_EDGE ( 'NONE', *, *, #10991, .F. ) ;
#12196=EDGE_CURVE ( 'NONE', #1325, #21072, #22535, .T. ) ;
#12197=CIRCLE ( 'NONE', #22091, 1.020000000000000018 ) ;
#12204=CARTESIAN_POINT ( 'NONE',  ( -3.458734125000000326, 0.000000000000000000, 5.737500001365596347 ) ) ;
#12206=DIRECTION ( 'NONE',  ( -0.000000000000000000, -0.000000000000000000, 1.000000000000000000 ) ) ;
#12212=CARTESIAN_POINT ( 'NONE',  ( -6.499999999999999112, 2.531211054341943711, -3.440493080744400967 ) ) ;
#12213=CARTESIAN_POINT ( 'NONE',  ( 7.347880794884118750E-16, -4.000000000000000000, -1.449999999999998179 ) ) ;
#12224=VECTOR ( 'NONE', #15647, 1000.000000000000000 ) ;
#12248=CARTESIAN_POINT ( 'NONE',  ( 6.499999999999999112, -3.752776749732574135, -0.5805565836007695601 ) ) ;
#12267=CARTESIAN_POINT ( 'NONE',  ( 1.432654583217642275, -3.458734124999999882, 1.300000001365597235 ) ) ;
#12268=DIRECTION ( 'NONE',  ( 1.000000000000000000, 0.000000000000000000, 0.000000000000000000 ) ) ;
#12272=AXIS2_PLACEMENT_3D ( 'NONE', #3980, #22291, #3735 ) ;
#12279=CARTESIAN_POINT ( 'NONE',  ( 3.458734125000000326, 1.432654583217640498, -2.699999998634404541 ) ) ;
#12283=AXIS2_PLACEMENT_3D ( 'NONE', #4814, #10359, #17649 ) ;
#12294=CARTESIAN_POINT ( 'NONE',  ( 4.000000000000000888, -1.656854249492379694, -2.137499997268812013 ) ) ;
#12299=CARTESIAN_POINT ( 'NONE',  ( -2.445694354108820523, 2.445694354108820523, 2.862500001365597235 ) ) ;
#12300=CARTESIAN_POINT ( 'NONE',  ( -1.722946112685674436, -3.007685260252270787, 2.039999999999996927 ) ) ;
#12301=EDGE_CURVE ( 'NONE', #14122, #18029, #3112, .T. ) ;
#12304=CARTESIAN_POINT ( 'NONE',  ( 0.000000000000000000, 0.000000000000000000, 0.000000000000000000 ) ) ;
#12307=CARTESIAN_POINT ( 'NONE',  ( -4.000000000000000000, 0.000000000000000000, -1.574999997268811569 ) ) ;
#12325=CARTESIAN_POINT ( 'NONE',  ( 3.458734125000000770, -1.432654583217639610, 4.175000001365593683 ) ) ;
#12333=( BOUNDED_CURVE ( )  B_SPLINE_CURVE ( 2, ( #52, #20148, #14693, #7496, #3881, #21949, #5921, #5562, #18491 ),
 .UNSPECIFIED., .F., .F. ) 
 B_SPLINE_CURVE_WITH_KNOTS ( ( 3, 2, 2, 2, 3 ),
 ( 0.8499999999999999778, 0.8625000000000000444, 0.8750000000000000000, 0.8874999999999999556, 0.9000000000000000222 ),
 .UNSPECIFIED. ) 
 CURVE ( )  GEOMETRIC_REPRESENTATION_ITEM ( )  RATIONAL_B_SPLINE_CURVE ( ( 1.000000000000000000, 0.9238795325112867385, 1.000000000000000000, 0.9238795325112867385, 1.000000000000000000, 0.9238795325112867385, 1.000000000000000000, 0.9238795325112867385, 1.000000000000000000 ) ) 
 REPRESENTATION_ITEM ( '' )  );
#12341=FACE_OUTER_BOUND ( 'NONE', #7436, .T. ) ;
#12345=CARTESIAN_POINT ( 'NONE',  ( -6.500000000000000000, 3.752776749732564809, -0.5805565836007661185 ) ) ;
#12348=CARTESIAN_POINT ( 'NONE',  ( 7.347880794884118750E-16, -4.000000000000000000, -0.4499999999999972911 ) ) ;
#12359=CARTESIAN_POINT ( 'NONE',  ( -4.000000000000000888, 1.656854249492380804, -1.762499999999997957 ) ) ;
#12365=CARTESIAN_POINT ( 'NONE',  ( 1.432654583217639832, 3.458734125000000326, -1.574999998634403875 ) ) ;
#12370=DIRECTION ( 'NONE',  ( 0.000000000000000000, 0.000000000000000000, -1.000000000000000000 ) ) ;
#12381=CARTESIAN_POINT ( 'NONE',  ( -2.445694354108819635, -2.445694354108820967, -0.8874999986344025427 ) ) ;
#12386=ORIENTED_EDGE ( 'NONE', *, *, #3532, .T. ) ;
#12392=CARTESIAN_POINT ( 'NONE',  ( -3.458734125000001214, 0.3674941000104132716, -3.278532042589525908 ) ) ;
#12409=CARTESIAN_POINT ( 'NONE',  ( 2.445694354108820967, -2.445694354108820079, 0.3625000013655968467 ) ) ;
#12414=CARTESIAN_POINT ( 'NONE',  ( -2.117863837641483646E-16, 3.458734125000000770, -3.295601554149324208 ) ) ;
#12418=CARTESIAN_POINT ( 'NONE',  ( -4.000000000000000888, 1.656854249492380804, 0.3625000027311864881 ) ) ;
#12429=DIRECTION ( 'NONE',  ( -1.000000000000000000, 0.000000000000000000, 0.000000000000000000 ) ) ;
#12434=DIRECTION ( 'NONE',  ( -1.000000000000000000, 0.000000000000000000, 0.000000000000000000 ) ) ;
#12437=CARTESIAN_POINT ( 'NONE',  ( -1.432654583217640276, 3.458734125000000326, 5.550000001365596347 ) ) ;
#12463=CARTESIAN_POINT ( 'NONE',  ( 0.000000000000000000, 0.000000000000000000, 0.000000000000000000 ) ) ;
#12465=CARTESIAN_POINT ( 'NONE',  ( 1.656854249492383024, -3.999999999999999112, -0.3874999999999968470 ) ) ;
#12468=( BOUNDED_CURVE ( )  B_SPLINE_CURVE ( 2, ( #21955, #16709, #2202, #11345, #14699, #23658, #5928, #7272, #22067, #13136, #16835, #2078, #9542, #5453, #14941, #7502, #5685, #414, #13257, #7743, #20283, #3763, #9418, #22196, #18260, #12788, #3885, #18383, #1845, #58, #1963, #20042, #10981, #12897, #5809, #15058, #13022, #14818, #9194, #11219, #20399, #5569, #20519, #4122, #16478, #22314, #16593, #11466, #18742, #7390, #20155, #11103, #15644, #4475, #2906, #22675, #642, #7850, #15175, #18968, #11584, #769, #2550, #13603, #2438, #22917, #17069, #6286, #17429, #22433, #8322, #9896, #4360, #2684, #11698, #6045, #8102, #17311, #11942, #21103, #12051, #10023, #6529, #20868, #22794, #10136, #15413 ),
 .UNSPECIFIED., .F., .F. ) 
 B_SPLINE_CURVE_WITH_KNOTS ( ( 3, 2, 2, 2, 2, 2, 2, 2, 2, 2, 2, 2, 2, 2, 2, 2, 2, 2, 2, 2, 2, 2, 2, 2, 2, 2, 2, 2, 2, 2, 2, 2, 2, 2, 2, 2, 2, 2, 2, 2, 2, 2, 2, 3 ),
 ( 0.3947128431780269620, 0.4000000000000000222, 0.4124999999999999778, 0.4249999999999999889, 0.4375000000000000000, 0.4500000000000000111, 0.4625000000000000222, 0.4749999999999999778, 0.4874999999999999889, 0.5000000000000000000, 0.5124999999999999556, 0.5250000000000000222, 0.5374999999999999778, 0.5500000000000000444, 0.5625000000000000000, 0.5749999999999999556, 0.5875000000000000222, 0.5999999999999999778, 0.6125000000000000444, 0.6250000000000000000, 0.6374999999999999556, 0.6500000000000000222, 0.6624999999999999778, 0.6750000000000000444, 0.6875000000000000000, 0.6999999999999999556, 0.7125000000000000222, 0.7249999999999999778, 0.7375000000000000444, 0.7500000000000000000, 0.7624999999999999556, 0.7750000000000000222, 0.7874999999999999778, 0.8000000000000000444, 0.8125000000000000000, 0.8249999999999999556, 0.8375000000000000222, 0.8499999999999999778, 0.8625000000000000444, 0.8750000000000000000, 0.8874999999999999556, 0.8999999999999999112, 0.9124999999999998668, 0.9250000000000000444 ),
 .UNSPECIFIED. ) 
 CURVE ( )  GEOMETRIC_REPRESENTATION_ITEM ( )  RATIONAL_B_SPLINE_CURVE ( ( 0.9628430465414361539, 0.9678031320820217331, 1.000000000000000000, 0.9238795325112867385, 1.000000000000000000, 0.9238795325112867385, 1.000000000000000000, 0.9238795325112867385, 1.000000000000000000, 0.9238795325112867385, 1.000000000000000000, 0.9238795325112867385, 1.000000000000000000, 0.9238795325112867385, 1.000000000000000000, 0.9238795325112867385, 1.000000000000000000, 0.9238795325112867385, 1.000000000000000000, 0.9238795325112867385, 1.000000000000000000, 0.9238795325112867385, 1.000000000000000000, 0.9238795325112867385, 1.000000000000000000, 0.9238795325112867385, 1.000000000000000000, 0.9238795325112867385, 1.000000000000000000, 0.9238795325112867385, 1.000000000000000000, 0.9238795325112867385, 1.000000000000000000, 0.9238795325112867385, 1.000000000000000000, 0.9238795325112867385, 1.000000000000000000, 0.9238795325112867385, 1.000000000000000000, 0.9238795325112867385, 1.000000000000000000, 0.9238795325112867385, 1.000000000000000000, 0.9238795325112867385, 1.000000000000000000, 0.9238795325112867385, 1.000000000000000000, 0.9238795325112867385, 1.000000000000000000, 0.9238795325112867385, 1.000000000000000000, 0.9238795325112867385, 1.000000000000000000, 0.9238795325112867385, 1.000000000000000000, 0.9238795325112867385, 1.000000000000000000, 0.9238795325112867385, 1.000000000000000000, 0.9238795325112867385, 1.000000000000000000, 0.9238795325112867385, 1.000000000000000000, 0.9238795325112867385, 1.000000000000000000, 0.9238795325112867385, 1.000000000000000000, 0.9238795325112867385, 1.000000000000000000, 0.9238795325112867385, 1.000000000000000000, 0.9238795325112867385, 1.000000000000000000, 0.9238795325112867385, 1.000000000000000000, 0.9238795325112867385, 1.000000000000000000, 0.9238795325112867385, 1.000000000000000000, 0.9238795325112867385, 1.000000000000000000, 0.9238795325112867385, 1.000000000000000000, 0.9238795325112867385, 1.000000000000000000, 0.9238795325112867385, 1.000000000000000000 ) ) 
 REPRESENTATION_ITEM ( '' )  );
#12481=CARTESIAN_POINT ( 'NONE',  ( 1.656854249492383024, -3.999999999999999112, 0.7375000027311867656 ) ) ;
#12485=CARTESIAN_POINT ( 'NONE',  ( 1.432654583217642275, -3.458734124999999437, -2.949999998634404985 ) ) ;
#12506=CARTESIAN_POINT ( 'NONE',  ( 1.432654583217640276, 3.458734125000000770, -0.3249999986344045411 ) ) ;
#12517=CARTESIAN_POINT ( 'NONE',  ( 3.458734125000000326, 1.432654583217640498, -1.699999998634403875 ) ) ;
#12541=ORIENTED_EDGE ( 'NONE', *, *, #11725, .T. ) ;
#12544=CARTESIAN_POINT ( 'NONE',  ( 4.000000000000000888, -1.656854249492379694, -0.1374999972688120964 ) ) ;
#12546=VERTEX_POINT ( 'NONE', #2923 ) ;
#12564=CARTESIAN_POINT ( 'NONE',  ( 6.353591512924457348E-16, -3.458734125000000326, 2.987500001365597235 ) ) ;
#12574=ORIENTED_EDGE ( 'NONE', *, *, #1907, .T. ) ;
#12576=ORIENTED_EDGE ( 'NONE', *, *, #14917, .T. ) ;
#12578=CARTESIAN_POINT ( 'NONE',  ( -5.007715329123867711E-16, -7.505553499465146494, -3.700000000000000178 ) ) ;
#12598=CARTESIAN_POINT ( 'NONE',  ( -1.067197363239236640, -6.889406814520513400, -0.2573354458087871444 ) ) ;
#12600=VERTEX_POINT ( 'NONE', #19285 ) ;
#12601=CARTESIAN_POINT ( 'NONE',  ( -0.1973187206307981389, 3.458734125000000326, -3.295601554149323764 ) ) ;
#12603=CARTESIAN_POINT ( 'NONE',  ( 0.000000000000000000, 0.000000000000000000, 2.039999999999998259 ) ) ;
#12608=CARTESIAN_POINT ( 'NONE',  ( 3.458734125000000326, 1.432654583217640498, -2.699999998634404541 ) ) ;
#12618=FACE_OUTER_BOUND ( 'NONE', #1627, .T. ) ;
#12620=DIRECTION ( 'NONE',  ( 1.000000000000000000, 0.000000000000000000, 0.000000000000000000 ) ) ;
#12629=CARTESIAN_POINT ( 'NONE',  ( 4.000000000000000000, 4.898587196589412829E-16, 4.800000000000000711 ) ) ;
#12637=VERTEX_POINT ( 'NONE', #19058 ) ;
#12642=CARTESIAN_POINT ( 'NONE',  ( -4.000000000000000000, 0.000000000000000000, -2.574999997268812457 ) ) ;
#12657=CARTESIAN_POINT ( 'NONE',  ( 6.353591512924457348E-16, -3.458734125000000770, -1.762499998634403209 ) ) ;
#12659=EDGE_CURVE ( 'NONE', #4081, #18467, #22964, .T. ) ;
#12666=ORIENTED_EDGE ( 'NONE', *, *, #10543, .F. ) ;
#12670=CARTESIAN_POINT ( 'NONE',  ( 3.458734125000000770, -1.432654583217639610, 5.175000001365595459 ) ) ;
#12676=CARTESIAN_POINT ( 'NONE',  ( 4.000000000000000000, 4.898587196589412829E-16, -3.074999997268812901 ) ) ;
#12689=CARTESIAN_POINT ( 'NONE',  ( 3.458734125000000770, -1.432654583217639610, -0.8249999986344030978 ) ) ;
#12704=DIRECTION ( 'NONE',  ( 1.000000000000000000, 0.000000000000000000, 0.000000000000000000 ) ) ;
#12705=ORIENTED_EDGE ( 'NONE', *, *, #247, .T. ) ;
#12706=EDGE_CURVE ( 'NONE', #3785, #15043, #22216, .T. ) ;
#12716=CARTESIAN_POINT ( 'NONE',  ( 2.149058192116893196, -6.264794173742287420, -3.633174458636617477 ) ) ;
#12719=DIRECTION ( 'NONE',  ( -0.000000000000000000, -0.000000000000000000, 1.000000000000000000 ) ) ;
#12738=EDGE_CURVE ( 'NONE', #10634, #438, #8087, .T. ) ;
#12741=CARTESIAN_POINT ( 'NONE',  ( -2.828427124746189403, -2.828427124746190735, -0.4499999972688122352 ) ) ;
#12744=CARTESIAN_POINT ( 'NONE',  ( 4.000000000000000000, 1.656854249492381248, 3.862500000000005151 ) ) ;
#12767=DIRECTION ( 'NONE',  ( -0.000000000000000000, -0.000000000000000000, 1.000000000000000000 ) ) ;
#12769=DIRECTION ( 'NONE',  ( -1.000000000000000000, 0.000000000000000000, 0.000000000000000000 ) ) ;
#12775=ORIENTED_EDGE ( 'NONE', *, *, #20736, .T. ) ;
#12777=CARTESIAN_POINT ( 'NONE',  ( 2.828427124746190735, -2.828427124746189847, -2.199999997268812013 ) ) ;
#12779=DIRECTION ( 'NONE',  ( -0.8660254037844382635, -0.5000000000000005551, 0.000000000000000000 ) ) ;
#12785=ORIENTED_EDGE ( 'NONE', *, *, #12196, .T. ) ;
#12788=CARTESIAN_POINT ( 'NONE',  ( 3.458734125000000770, 1.432654583217640498, 0.5500000013655963471 ) ) ;
#12796=CARTESIAN_POINT ( 'NONE',  ( -1.432654583217640942, -3.458734124999999882, 0.9250000013655964581 ) ) ;
#12817=CARTESIAN_POINT ( 'NONE',  ( -2.828427124746189403, -2.828427124746190735, -0.5749999999999974021 ) ) ;
#12822=CARTESIAN_POINT ( 'NONE',  ( 3.548171615569589044, -1.118847994424759351, 2.039999999999997371 ) ) ;
#12825=CARTESIAN_POINT ( 'NONE',  ( 6.499999999999999112, -3.752776749732574135, -3.119443416399232394 ) ) ;
#12827=CARTESIAN_POINT ( 'NONE',  ( -0.7789945309248447192, 3.375565665863409670, -3.295601554149322432 ) ) ;
#12831=DIRECTION ( 'NONE',  ( 1.000000000000000000, 0.000000000000000000, 0.000000000000000000 ) ) ;
#12832=CARTESIAN_POINT ( 'NONE',  ( -2.445694354108820523, 2.445694354108820523, -2.387499998634403653 ) ) ;
#12838=EDGE_LOOP ( 'NONE', ( #15358, #5974, #20856, #14273, #20410, #13304 ) ) ;
#12839=CARTESIAN_POINT ( 'NONE',  ( -1.656854249492381248, -3.999999999999999112, 1.487500000000001155 ) ) ;
#12852=CARTESIAN_POINT ( 'NONE',  ( -4.000000000000000888, 1.656854249492380804, 6.237500000000001599 ) ) ;
#12876=LINE ( 'NONE', #14676, #9121 ) ;
#12887=CARTESIAN_POINT ( 'NONE',  ( -1.656854249492381248, -3.999999999999999112, -2.387499997268812013 ) ) ;
#12889=CARTESIAN_POINT ( 'NONE',  ( -5.969670414742689779, -4.058962678540106062, -0.4037800551813781058 ) ) ;
#12890=ORIENTED_EDGE ( 'NONE', *, *, #11264, .F. ) ;
#12897=CARTESIAN_POINT ( 'NONE',  ( -3.458734125000000326, -1.432654583217642497, 0.05000000136559583364 ) ) ;
#12904=CARTESIAN_POINT ( 'NONE',  ( -2.117863837641485618E-16, 3.458734125000000326, -0.5124999986344038749 ) ) ;
#12909=EDGE_LOOP ( 'NONE', ( #21862, #20537 ) ) ;
#12917=B_SPLINE_CURVE_WITH_KNOTS ( 'NONE', 3,
 ( #5559, #13009, #18731, #16583, #16828, #2320, #12889, #3749 ),
 .UNSPECIFIED., .F., .F.,
 ( 4, 2, 2, 4 ),
 ( 0.003797433802554454115, 0.004743183970586247432, 0.005688934138618041182, 0.007580434474681629550 ),
 .UNSPECIFIED. ) ;
#12934=CARTESIAN_POINT ( 'NONE',  ( -2.117863837641482907E-16, 3.458734125000000770, -3.284567702311016468 ) ) ;
#12946=EDGE_CURVE ( 'NONE', #11906, #438, #1356, .T. ) ;
#12948=CARTESIAN_POINT ( 'NONE',  ( 0.000000000000000000, 0.000000000000000000, 19.04999999999996874 ) ) ;
#12950=CARTESIAN_POINT ( 'NONE',  ( -4.000000000000000000, 4.898587196589412829E-16, 19.04999999999996874 ) ) ;
#12962=MECHANICAL_DESIGN_GEOMETRIC_PRESENTATION_REPRESENTATION('',(#14103),#18281);
#12967=LINE ( 'NONE', #1916, #9924 ) ;
#12971=AXIS2_PLACEMENT_3D ( 'NONE', #21668, #8894, #16188 ) ;
#12972=CARTESIAN_POINT ( 'NONE',  ( 1.432654583217640276, 3.458734125000000770, -2.324999998634404097 ) ) ;
#12995=PLANE ( 'NONE',  #12272 ) ;
#12999=AXIS2_PLACEMENT_3D ( 'NONE', #16535, #111, #21545 ) ;
#13007=SURFACE_SIDE_STYLE ('',( #9651 ) ) ;
#13008=CARTESIAN_POINT ( 'NONE',  ( -2.449293598294706907E-16, 4.000000000000000000, -1.824999997268811791 ) ) ;
#13009=CARTESIAN_POINT ( 'NONE',  ( -3.525817189091417170, -5.469921996229802907, 4.020583056300408003E-16 ) ) ;
#13014=CARTESIAN_POINT ( 'NONE',  ( -2.117863837641485618E-16, 3.458734125000000770, -3.262499998634402765 ) ) ;
#13022=CARTESIAN_POINT ( 'NONE',  ( -2.445694354108820523, 2.445694354108820523, -0.1374999986344035974 ) ) ;
#13029=CARTESIAN_POINT ( 'NONE',  ( -1.432654583217640942, -3.458734124999999882, 1.925000001365597457 ) ) ;
#13035=CARTESIAN_POINT ( 'NONE',  ( 6.500000000000000888, -2.517290933526018737, -3.443420074781601059 ) ) ;
#13058=CARTESIAN_POINT ( 'NONE',  ( 1.656854249492380138, 4.000000000000000000, 0.1125000027311862244 ) ) ;
#13060=CARTESIAN_POINT ( 'NONE',  ( 3.736776272708129287, -0.5369652245313190075, 2.039999999999999147 ) ) ;
#13064=CARTESIAN_POINT ( 'NONE',  ( -2.697128823393878161, 5.948365447239581272, -0.01372220897661629788 ) ) ;
#13069=ORIENTED_EDGE ( 'NONE', *, *, #15414, .T. ) ;
#13093=B_SPLINE_CURVE_WITH_KNOTS ( 'NONE', 3,
 ( #17126, #7798, #15115, #11878, #4893, #19607 ),
 .UNSPECIFIED., .F., .F.,
 ( 4, 2, 4 ),
 ( 0.01049192114530184475, 0.01239128608052813933, 0.01429065101575443392 ),
 .UNSPECIFIED. ) ;
#13094=CARTESIAN_POINT ( 'NONE',  ( 3.458734125000001214, -1.432654583217639610, -1.574999998634403875 ) ) ;
#13095=CARTESIAN_POINT ( 'NONE',  ( -4.000000000000000000, -1.656854249492383246, 4.362500000000001599 ) ) ;
#13127=CARTESIAN_POINT ( 'NONE',  ( -1.432654583217640942, -3.458734124999999882, 4.925000001365594571 ) ) ;
#13136=CARTESIAN_POINT ( 'NONE',  ( 3.458734125000000770, 1.432654583217640498, 1.550000001365597013 ) ) ;
#13141=CARTESIAN_POINT ( 'NONE',  ( -3.458734124999999882, -1.432654583217642497, -3.199999998634404985 ) ) ;
#13152=ORIENTED_EDGE ( 'NONE', *, *, #9243, .F. ) ;
#13162=B_SPLINE_CURVE_WITH_KNOTS ( 'NONE', 3,
 ( #8529, #15833, #14028, #21291, #14867, #3931 ),
 .UNSPECIFIED., .F., .F.,
 ( 4, 2, 4 ),
 ( 0.01049192114530184301, 0.01239128608052813413, 0.01429065101575442351 ),
 .UNSPECIFIED. ) ;
#13169=CARTESIAN_POINT ( 'NONE',  ( 2.244686410773148566, -2.775871127258929594, 2.039999999999996927 ) ) ;
#13190=EDGE_CURVE ( 'NONE', #12546, #2635, #21681, .T. ) ;
#13204=CARTESIAN_POINT ( 'NONE',  ( 2.445694354108820079, 2.445694354108820523, -1.387499998634402987 ) ) ;
#13205=CARTESIAN_POINT ( 'NONE',  ( -4.000000000000000000, 0.000000000000000000, 0.3000000000000016542 ) ) ;
#13210=VERTEX_POINT ( 'NONE', #19468 ) ;
#13215=PRODUCT_CONTEXT ( 'NONE', #9014, 'mechanical' ) ;
#13224=VECTOR ( 'NONE', #7161, 1000.000000000000000 ) ;
#13225=AXIS2_PLACEMENT_3D ( 'NONE', #12948, #19866, #12831 ) ;
#13230=CARTESIAN_POINT ( 'NONE',  ( 6.499999999999999112, -3.752776749732574135, -0.5805565836007695601 ) ) ;
#13234=CARTESIAN_POINT ( 'NONE',  ( 3.458734125000000770, 1.432654583217640498, 2.550000001365598123 ) ) ;
#13238=VERTEX_POINT ( 'NONE', #21368 ) ;
#13243=FILL_AREA_STYLE_COLOUR ( '', #17547 ) ;
#13244=CARTESIAN_POINT ( 'NONE',  ( 3.458734125000000326, 4.235727675282971730E-16, 1.237500001365595903 ) ) ;
#13257=CARTESIAN_POINT ( 'NONE',  ( -3.458734125000000770, 0.000000000000000000, 0.9875000013655956810 ) ) ;
#13262=CARTESIAN_POINT ( 'NONE',  ( 1.432654583217642275, -3.458734124999999882, 4.300000001365595459 ) ) ;
#13291=CARTESIAN_POINT ( 'NONE',  ( 4.000000000000000000, 4.898587196589412829E-16, 0.8000000000000020428 ) ) ;
#13303=CARTESIAN_POINT ( 'NONE',  ( 3.250000000000003109, 5.629165124598848102, 1.734723475976807094E-15 ) ) ;
#13304=ORIENTED_EDGE ( 'NONE', *, *, #11465, .F. ) ;
#13310=CARTESIAN_POINT ( 'NONE',  ( 2.696295709017754838, 5.948846446048901448, -3.700000000000005063 ) ) ;
#13319=EDGE_CURVE ( 'NONE', #1325, #15816, #12468, .T. ) ;
#13323=CARTESIAN_POINT ( 'NONE',  ( 2.445694354108820967, -2.445694354108820079, -1.637499998634403209 ) ) ;
#13324=CARTESIAN_POINT ( 'NONE',  ( 4.000000000000000888, -1.656854249492379694, 1.737500000000001377 ) ) ;
#13337=ORIENTED_EDGE ( 'NONE', *, *, #2604, .F. ) ;
#13354=CARTESIAN_POINT ( 'NONE',  ( 2.445694354108820079, 2.445694354108820523, 2.612500001365597235 ) ) ;
#13362=CARTESIAN_POINT ( 'NONE',  ( 3.458734125000000326, 1.432654583217640498, 1.300000001365597235 ) ) ;
#13368=CARTESIAN_POINT ( 'NONE',  ( 0.000000000000000000, 0.000000000000000000, -3.699999999999998401 ) ) ;
#13378=CIRCLE ( 'NONE', #19467, 6.500000000000000888 ) ;
#13382=AXIS2_PLACEMENT_3D ( 'NONE', #15203, #18997, #16872 ) ;
#13385=CARTESIAN_POINT ( 'NONE',  ( 2.445694354108820079, 2.445694354108820523, -2.637499998634404097 ) ) ;
#13394=CARTESIAN_POINT ( 'NONE',  ( 4.000000000000000000, 1.656854249492381248, 4.987500002731185766 ) ) ;
#13441=ORIENTED_EDGE ( 'NONE', *, *, #5565, .F. ) ;
#13443=CARTESIAN_POINT ( 'NONE',  ( 6.500000000000000000, 3.752776749732573247, -0.5805565836007695601 ) ) ;
#13449=CARTESIAN_POINT ( 'NONE',  ( 1.656854249492383024, -3.999999999999999112, -0.3874999999999967915 ) ) ;
#13452=CARTESIAN_POINT ( 'NONE',  ( 4.000000000000000000, 1.656854249492381248, -1.137499999999997513 ) ) ;
#13474=CARTESIAN_POINT ( 'NONE',  ( 3.458734125000000770, 4.235727675282972223E-16, 5.487500001365596347 ) ) ;
#13480=DIRECTION ( 'NONE',  ( 1.000000000000000000, 0.000000000000000000, 0.000000000000000000 ) ) ;
#13483=CARTESIAN_POINT ( 'NONE',  ( -3.458734125000000326, 0.000000000000000000, 2.737500001365597235 ) ) ;
#13484=EDGE_CURVE ( 'NONE', #4626, #1632, #17373, .T. ) ;
#13485=CARTESIAN_POINT ( 'NONE',  ( -3.458734125000000326, 0.000000000000000000, -0.2624999986344037084 ) ) ;
#13488=DIRECTION ( 'NONE',  ( 1.000000000000000000, 0.000000000000000000, 0.000000000000000000 ) ) ;
#13501=CARTESIAN_POINT ( 'NONE',  ( 1.432654583217640276, 3.458734125000000770, 4.675000001365594571 ) ) ;
#13505=CARTESIAN_POINT ( 'NONE',  ( -4.000000000000000000, 0.000000000000000000, -1.699999999999998401 ) ) ;
#13508=CARTESIAN_POINT ( 'NONE',  ( -2.449293598294706907E-16, 4.000000000000000000, 5.175000002731187543 ) ) ;
#13521=DIRECTION ( 'NONE',  ( 1.000000000000000000, 0.000000000000000000, 0.000000000000000000 ) ) ;
#13534=CARTESIAN_POINT ( 'NONE',  ( 0.000000000000000000, 0.000000000000000000, -3.700000000000000178 ) ) ;
#13558=CARTESIAN_POINT ( 'NONE',  ( 4.000000000000000888, -1.656854249492379694, 0.7375000000000022649 ) ) ;
#13574=PRODUCT_DEFINITION ( 'UNKNOWN', '', #3796, #22948 ) ;
#13583=CARTESIAN_POINT ( 'NONE',  ( 3.458734125000000770, 4.235727675282972223E-16, 2.487500001365596791 ) ) ;
#13593=CARTESIAN_POINT ( 'NONE',  ( -2.117863837641485618E-16, 3.458734125000000326, 3.487500001365594571 ) ) ;
#13598=SURFACE_STYLE_USAGE ( .BOTH. , #9890 ) ;
#13603=CARTESIAN_POINT ( 'NONE',  ( -1.432654583217641164, -3.458734125000000326, -1.824999998634404097 ) ) ;
#13613=AXIS2_PLACEMENT_3D ( 'NONE', #13992, #12206, #1972 ) ;
#13614=CARTESIAN_POINT ( 'NONE',  ( 3.458734125000000326, 1.432654583217640498, -2.699999998634404541 ) ) ;
#13623=CARTESIAN_POINT ( 'NONE',  ( 2.828427124746190735, -2.828427124746189847, 3.800000002731186211 ) ) ;
#13643=ADVANCED_FACE ( 'NONE', ( #11531 ), #6794, .T. ) ;
#13644=CARTESIAN_POINT ( 'NONE',  ( 0.000000000000000000, 0.000000000000000000, -3.700000000000000178 ) ) ;
#13656=CARTESIAN_POINT ( 'NONE',  ( -2.828427124746190291, 2.828427124746190291, 1.175000000000000711 ) ) ;
#13672=CARTESIAN_POINT ( 'NONE',  ( 0.000000000000000000, 0.000000000000000000, -3.699999999999998401 ) ) ;
#13676=CARTESIAN_POINT ( 'NONE',  ( 1.656854249492380360, 4.000000000000000000, -0.01249999999999832322 ) ) ;
#13683=VECTOR ( 'NONE', #16112, 1000.000000000000000 ) ;
#13686=CARTESIAN_POINT ( 'NONE',  ( -2.449293598294706907E-16, 4.000000000000000000, -1.824999997268811791 ) ) ;
#13700=AXIS2_PLACEMENT_3D ( 'NONE', #6531, #17314, #8106 ) ;
#13701=CARTESIAN_POINT ( 'NONE',  ( 1.432654583217640276, 3.458734125000000770, 3.675000001365597235 ) ) ;
#13704=PLANE ( 'NONE',  #12283 ) ;
#13709=EDGE_LOOP ( 'NONE', ( #6038, #12192, #22754, #3780, #22789 ) ) ;
#13711=CARTESIAN_POINT ( 'NONE',  ( -1.432654583217640942, -3.458734124999999882, 0.9250000013655964581 ) ) ;
#13712=CARTESIAN_POINT ( 'NONE',  ( 3.458734125000000326, 1.432654583217640498, 0.3000000013655960140 ) ) ;
#13716=DIRECTION ( 'NONE',  ( -0.000000000000000000, -0.000000000000000000, 1.000000000000000000 ) ) ;
#13719=ORIENTED_EDGE ( 'NONE', *, *, #23438, .T. ) ;
#13722=( BOUNDED_CURVE ( )  B_SPLINE_CURVE ( 2, ( #5621, #21041, #13656, #11637, #9600, #15222, #8150, #19143, #22487 ),
 .UNSPECIFIED., .F., .F. ) 
 B_SPLINE_CURVE_WITH_KNOTS ( ( 3, 2, 2, 2, 3 ),
 ( 0.5000000000000000000, 0.5124999999999999556, 0.5250000000000000222, 0.5374999999999999778, 0.5500000000000000444 ),
 .UNSPECIFIED. ) 
 CURVE ( )  GEOMETRIC_REPRESENTATION_ITEM ( )  RATIONAL_B_SPLINE_CURVE ( ( 1.000000000000000000, 0.9238795325112867385, 1.000000000000000000, 0.9238795325112867385, 1.000000000000000000, 0.9238795325112867385, 1.000000000000000000, 0.9238795325112867385, 1.000000000000000000 ) ) 
 REPRESENTATION_ITEM ( '' )  );
#13732=CARTESIAN_POINT ( 'NONE',  ( 3.458734125000000770, 1.432654583217640498, 0.5500000013655963471 ) ) ;
#13741=CARTESIAN_POINT ( 'NONE',  ( -1.656854249492381248, -3.999999999999999112, 2.612500002731188431 ) ) ;
#13745=CARTESIAN_POINT ( 'NONE',  ( -4.000000000000000000, -1.656854249492383024, 1.487500002731187321 ) ) ;
#13782=CARTESIAN_POINT ( 'NONE',  ( 1.067197363239223762, 6.889406814520512512, -0.2573354458087852570 ) ) ;
#13801=AXIS2_PLACEMENT_3D ( 'NONE', #1093, #21200, #8547 ) ;
#13803=CARTESIAN_POINT ( 'NONE',  ( -1.857128706618043301, 2.924396244061969519, -3.295601554149324208 ) ) ;
#13815=EDGE_CURVE ( 'NONE', #5142, #19833, #8389, .T. ) ;
#13828=CARTESIAN_POINT ( 'NONE',  ( -3.458734125000000770, 0.000000000000000000, -1.012499998634402543 ) ) ;
#13839=CARTESIAN_POINT ( 'NONE',  ( 3.458734125000000326, 4.235727675282971730E-16, -0.7624999986344040970 ) ) ;
#13856=CARTESIAN_POINT ( 'NONE',  ( 3.458734125000001214, -1.432654583217639610, 3.425000001365596791 ) ) ;
#13858=DIRECTION ( 'NONE',  ( 0.000000000000000000, 0.000000000000000000, 1.000000000000000000 ) ) ;
#13865=CARTESIAN_POINT ( 'NONE',  ( -2.449293598294706907E-16, 4.000000000000000000, 4.175000002731186655 ) ) ;
#13880=CARTESIAN_POINT ( 'NONE',  ( -1.432654583217640276, 3.458734125000000326, 3.550000001365595459 ) ) ;
#13889=ORIENTED_EDGE ( 'NONE', *, *, #10956, .F. ) ;
#13898=( BOUNDED_SURFACE ( )  B_SPLINE_SURFACE ( 1, 2, ( 
 ( #7599, #22175, #5790, #3983, #20500, #9642, #11445, #4583, #13474, #4340, #8303, #22414, #7952, #11919, #17405, #2773, #2308, #19187, #11679, #18948, #624, #6383, #15272, #6025, #17292, #2533, #5908, #11566, #8083, #17049, #15393, #9874, #16933, #18718, #22773, #4105, #17169, #13701, #20964, #857, #10113, #973, #15625, #747, #6151, #15153, #22656, #6265, #20735, #22543, #509, #4457, #7832, #4228, #13354, #13234, #13583, #2659, #20621, #18834, #20850, #2420, #11797, #8191, #9751, #19069, #10001, #15504, #21434, #6509, #1319, #4932, #8433, #3247, #19408, #12267, #23370, #4696, #14291, #8543, #10355, #8658, #17645, #6973, #21084, #5048, #23015, #12031, #6737, #3366, #21552, #14044, #15745, #17752, #2885, #19294, #19646, #10710, #6620, #17987, #5164, #12506, #1563, #15850, #10593, #1206, #19764, #8901, #22895, #17522, #12381, #13938, #13828, #10232, #23122, #21309, #19533, #3131, #1089, #10471, #15958, #21196, #4810, #17865, #16082, #12141, #3005, #23239, #6849, #14174, #1439, #8778, #3711, #12972, #9145, #5638, #19995, #14537, #18216, #18452, #3843, #11053, #21910, #21802, #20109, #9372, #21675, #5517, #5767 ),
 ( #16432, #12852, #237, #13, #1920, #9261, #16197, #10825, #11179, #18566, #7454, #23483, #16547, #11291, #7222, #20237, #123, #23607, #14769, #16662, #2031, #14890, #5284, #7571, #12629, #5407, #22023, #22148, #1797, #18340, #3490, #13095, #20350, #2149, #3957, #9024, #7096, #14413, #16317, #12744, #3598, #19889, #18100, #10937, #7345, #1680, #14652, #22510, #9844, #6361, #7922, #22634, #2629, #4316, #5997, #19039, #11770, #15015, #20593, #4077, #11892, #18690, #2394, #20827, #9973, #4200, #11414, #15242, #22387, #597, #9727, #365, #17266, #13324, #2280, #9484, #9618, #19161, #7698, #17140, #16784, #16908, #4436, #22269, #717, #5881, #8053, #4555, #486, #13558, #18924, #7809, #15367, #834, #8166, #15479, #13205, #22749, #20471, #15126, #6238, #13676, #11542, #6120, #18811, #20938, #17022, #13449, #20712, #11655, #2510, #10088, #2859, #22991, #8405, #19511, #3108, #21170, #1064, #4669, #19270, #15825, #10449, #23346, #1185, #15934, #19620, #21283, #6596, #12359, #5028, #8283, #13913, #21058, #5139, #12004, #19382, #14146, #3218, #4783, #10209, #8521, #15721, #17623, #2977, #17377, #10567, #12119, #17497 ) ),
 .UNSPECIFIED., .F., .F., .F. ) 
 B_SPLINE_SURFACE_WITH_KNOTS ( ( 2, 2 ),
 ( 3, 2, 2, 2, 2, 2, 2, 2, 2, 2, 2, 2, 2, 2, 2, 2, 2, 2, 2, 2, 2, 2, 2, 2, 2, 2, 2, 2, 2, 2, 2, 2, 2, 2, 2, 2, 2, 2, 2, 2, 2, 2, 2, 2, 2, 2, 2, 2, 2, 2, 2, 2, 2, 2, 2, 2, 2, 2, 2, 2, 2, 2, 2, 2, 2, 2, 2, 2, 2, 2, 2, 2, 2, 2, 3 ),
 ( 0.000000000000000000, 1.000000000000000000 ),
 ( 0.000000000000000000, 0.01250000000000000069, 0.02500000000000000139, 0.03749999999999999861, 0.05000000000000000278, 0.06250000000000000000, 0.07499999999999999722, 0.08749999999999999445, 0.1000000000000000056, 0.1125000000000000028, 0.1250000000000000000, 0.1375000000000000111, 0.1499999999999999944, 0.1625000000000000056, 0.1749999999999999889, 0.1875000000000000000, 0.2000000000000000111, 0.2124999999999999944, 0.2250000000000000056, 0.2374999999999999889, 0.2500000000000000000, 0.2625000000000000111, 0.2750000000000000222, 0.2874999999999999778, 0.2999999999999999889, 0.3125000000000000000, 0.3250000000000000111, 0.3375000000000000222, 0.3499999999999999778, 0.3624999999999999889, 0.3750000000000000000, 0.3875000000000000111, 0.4000000000000000222, 0.4124999999999999778, 0.4249999999999999889, 0.4375000000000000000, 0.4500000000000000111, 0.4625000000000000222, 0.4749999999999999778, 0.4874999999999999889, 0.5000000000000000000, 0.5124999999999999556, 0.5250000000000000222, 0.5374999999999999778, 0.5500000000000000444, 0.5625000000000000000, 0.5749999999999999556, 0.5875000000000000222, 0.5999999999999999778, 0.6125000000000000444, 0.6250000000000000000, 0.6374999999999999556, 0.6500000000000000222, 0.6624999999999999778, 0.6750000000000000444, 0.6875000000000000000, 0.6999999999999999556, 0.7125000000000000222, 0.7249999999999999778, 0.7375000000000000444, 0.7500000000000000000, 0.7624999999999999556, 0.7750000000000000222, 0.7874999999999999778, 0.8000000000000000444, 0.8125000000000000000, 0.8249999999999999556, 0.8375000000000000222, 0.8499999999999999778, 0.8625000000000000444, 0.8750000000000000000, 0.8874999999999999556, 0.9000000000000000222, 0.9124999999999999778, 0.9250000000000000444 ),
 .UNSPECIFIED. ) 
 GEOMETRIC_REPRESENTATION_ITEM ( )  RATIONAL_B_SPLINE_SURFACE ( (
 ( 1.000000000000000000, 0.9238795325112867385, 1.000000000000000000, 0.9238795325112867385, 1.000000000000000000, 0.9238795325112867385, 1.000000000000000000, 0.9238795325112867385, 1.000000000000000000, 0.9238795325112867385, 1.000000000000000000, 0.9238795325112867385, 1.000000000000000000, 0.9238795325112867385, 1.000000000000000000, 0.9238795325112867385, 1.000000000000000000, 0.9238795325112867385, 1.000000000000000000, 0.9238795325112867385, 1.000000000000000000, 0.9238795325112867385, 1.000000000000000000, 0.9238795325112867385, 1.000000000000000000, 0.9238795325112867385, 1.000000000000000000, 0.9238795325112867385, 1.000000000000000000, 0.9238795325112867385, 1.000000000000000000, 0.9238795325112867385, 1.000000000000000000, 0.9238795325112867385, 1.000000000000000000, 0.9238795325112867385, 1.000000000000000000, 0.9238795325112867385, 1.000000000000000000, 0.9238795325112867385, 1.000000000000000000, 0.9238795325112867385, 1.000000000000000000, 0.9238795325112867385, 1.000000000000000000, 0.9238795325112867385, 1.000000000000000000, 0.9238795325112867385, 1.000000000000000000, 0.9238795325112867385, 1.000000000000000000, 0.9238795325112867385, 1.000000000000000000, 0.9238795325112867385, 1.000000000000000000, 0.9238795325112867385, 1.000000000000000000, 0.9238795325112867385, 1.000000000000000000, 0.9238795325112867385, 1.000000000000000000, 0.9238795325112867385, 1.000000000000000000, 0.9238795325112867385, 1.000000000000000000, 0.9238795325112867385, 1.000000000000000000, 0.9238795325112867385, 1.000000000000000000, 0.9238795325112867385, 1.000000000000000000, 0.9238795325112867385, 1.000000000000000000, 0.9238795325112867385, 1.000000000000000000, 0.9238795325112867385, 1.000000000000000000, 0.9238795325112867385, 1.000000000000000000, 0.9238795325112867385, 1.000000000000000000, 0.9238795325112867385, 1.000000000000000000, 0.9238795325112867385, 1.000000000000000000, 0.9238795325112867385, 1.000000000000000000, 0.9238795325112867385, 1.000000000000000000, 0.9238795325112867385, 1.000000000000000000, 0.9238795325112867385, 1.000000000000000000, 0.9238795325112867385, 1.000000000000000000, 0.9238795325112867385, 1.000000000000000000, 0.9238795325112867385, 1.000000000000000000, 0.9238795325112867385, 1.000000000000000000, 0.9238795325112867385, 1.000000000000000000, 0.9238795325112867385, 1.000000000000000000, 0.9238795325112867385, 1.000000000000000000, 0.9238795325112867385, 1.000000000000000000, 0.9238795325112867385, 1.000000000000000000, 0.9238795325112867385, 1.000000000000000000, 0.9238795325112867385, 1.000000000000000000, 0.9238795325112867385, 1.000000000000000000, 0.9238795325112867385, 1.000000000000000000, 0.9238795325112867385, 1.000000000000000000, 0.9238795325112867385, 1.000000000000000000, 0.9238795325112867385, 1.000000000000000000, 0.9238795325112867385, 1.000000000000000000, 0.9238795325112867385, 1.000000000000000000, 0.9238795325112867385, 1.000000000000000000, 0.9238795325112867385, 1.000000000000000000, 0.9238795325112867385, 1.000000000000000000, 0.9238795325112867385, 1.000000000000000000, 0.9238795325112867385, 1.000000000000000000, 0.9238795325112867385, 1.000000000000000000, 0.9238795325112867385, 1.000000000000000000, 0.9238795325112867385, 1.000000000000000000, 0.9238795325112867385, 1.000000000000000000, 0.9238795325112867385, 1.000000000000000000),
 ( 1.000000000000000000, 0.9238795325112867385, 1.000000000000000000, 0.9238795325112867385, 1.000000000000000000, 0.9238795325112867385, 1.000000000000000000, 0.9238795325112867385, 1.000000000000000000, 0.9238795325112867385, 1.000000000000000000, 0.9238795325112867385, 1.000000000000000000, 0.9238795325112867385, 1.000000000000000000, 0.9238795325112867385, 1.000000000000000000, 0.9238795325112867385, 1.000000000000000000, 0.9238795325112867385, 1.000000000000000000, 0.9238795325112867385, 1.000000000000000000, 0.9238795325112867385, 1.000000000000000000, 0.9238795325112867385, 1.000000000000000000, 0.9238795325112867385, 1.000000000000000000, 0.9238795325112867385, 1.000000000000000000, 0.9238795325112867385, 1.000000000000000000, 0.9238795325112867385, 1.000000000000000000, 0.9238795325112867385, 1.000000000000000000, 0.9238795325112867385, 1.000000000000000000, 0.9238795325112867385, 1.000000000000000000, 0.9238795325112867385, 1.000000000000000000, 0.9238795325112867385, 1.000000000000000000, 0.9238795325112867385, 1.000000000000000000, 0.9238795325112867385, 1.000000000000000000, 0.9238795325112867385, 1.000000000000000000, 0.9238795325112867385, 1.000000000000000000, 0.9238795325112867385, 1.000000000000000000, 0.9238795325112867385, 1.000000000000000000, 0.9238795325112867385, 1.000000000000000000, 0.9238795325112867385, 1.000000000000000000, 0.9238795325112867385, 1.000000000000000000, 0.9238795325112867385, 1.000000000000000000, 0.9238795325112867385, 1.000000000000000000, 0.9238795325112867385, 1.000000000000000000, 0.9238795325112867385, 1.000000000000000000, 0.9238795325112867385, 1.000000000000000000, 0.9238795325112867385, 1.000000000000000000, 0.9238795325112867385, 1.000000000000000000, 0.9238795325112867385, 1.000000000000000000, 0.9238795325112867385, 1.000000000000000000, 0.9238795325112867385, 1.000000000000000000, 0.9238795325112867385, 1.000000000000000000, 0.9238795325112867385, 1.000000000000000000, 0.9238795325112867385, 1.000000000000000000, 0.9238795325112867385, 1.000000000000000000, 0.9238795325112867385, 1.000000000000000000, 0.9238795325112867385, 1.000000000000000000, 0.9238795325112867385, 1.000000000000000000, 0.9238795325112867385, 1.000000000000000000, 0.9238795325112867385, 1.000000000000000000, 0.9238795325112867385, 1.000000000000000000, 0.9238795325112867385, 1.000000000000000000, 0.9238795325112867385, 1.000000000000000000, 0.9238795325112867385, 1.000000000000000000, 0.9238795325112867385, 1.000000000000000000, 0.9238795325112867385, 1.000000000000000000, 0.9238795325112867385, 1.000000000000000000, 0.9238795325112867385, 1.000000000000000000, 0.9238795325112867385, 1.000000000000000000, 0.9238795325112867385, 1.000000000000000000, 0.9238795325112867385, 1.000000000000000000, 0.9238795325112867385, 1.000000000000000000, 0.9238795325112867385, 1.000000000000000000, 0.9238795325112867385, 1.000000000000000000, 0.9238795325112867385, 1.000000000000000000, 0.9238795325112867385, 1.000000000000000000, 0.9238795325112867385, 1.000000000000000000, 0.9238795325112867385, 1.000000000000000000, 0.9238795325112867385, 1.000000000000000000, 0.9238795325112867385, 1.000000000000000000, 0.9238795325112867385, 1.000000000000000000, 0.9238795325112867385, 1.000000000000000000, 0.9238795325112867385, 1.000000000000000000, 0.9238795325112867385, 1.000000000000000000) ) ) 
 REPRESENTATION_ITEM ( '' )  SURFACE ( )  );
#13911=CARTESIAN_POINT ( 'NONE',  ( 6.499999999999999112, 3.145973671264227889, -0.4053876232513715649 ) ) ;
#13913=CARTESIAN_POINT ( 'NONE',  ( -2.449293598294706907E-16, 4.000000000000000000, -1.949999999999998623 ) ) ;
#13936=CARTESIAN_POINT ( 'NONE',  ( 6.499999999999999112, -1.264206540070616835, -0.05450957050772529261 ) ) ;
#13938=CARTESIAN_POINT ( 'NONE',  ( -3.458734125000000326, -1.432654583217642497, -0.9499999986344030978 ) ) ;
#13950=CARTESIAN_POINT ( 'NONE',  ( -1.432654583217640276, 3.458734125000000326, 1.550000001365597013 ) ) ;
#13951=ORIENTED_EDGE ( 'NONE', *, *, #6502, .T. ) ;
#13952=DIRECTION ( 'NONE',  ( 1.224646799147353207E-16, 1.000000000000000000, 0.000000000000000000 ) ) ;
#13966=CARTESIAN_POINT ( 'NONE',  ( 3.458734125000001214, -1.432654583217639610, 0.4250000013655961251 ) ) ;
#13977=CARTESIAN_POINT ( 'NONE',  ( -2.828427124746189403, -2.828427124746190735, 0.5500000027311869877 ) ) ;
#13979=ORIENTED_EDGE ( 'NONE', *, *, #11754, .T. ) ;
#13990=CARTESIAN_POINT ( 'NONE',  ( 3.458734125000000326, 4.235727675282971730E-16, 4.237500001365595459 ) ) ;
#13992=CARTESIAN_POINT ( 'NONE',  ( 0.000000000000000000, 0.000000000000000000, 19.04999999999996874 ) ) ;
#13994=EDGE_LOOP ( 'NONE', ( #2952, #8373, #15336, #4521, #17033, #4642 ) ) ;
#13997=CARTESIAN_POINT ( 'NONE',  ( 0.000000000000000000, 0.000000000000000000, -3.700000000000000178 ) ) ;
#13998=CARTESIAN_POINT ( 'NONE',  ( 4.000000000000000000, 4.898587196589412829E-16, -1.199999999999997957 ) ) ;
#14006=CARTESIAN_POINT ( 'NONE',  ( 0.000000000000000000, 0.000000000000000000, 9.480888224575631185 ) ) ;
#14016=CARTESIAN_POINT ( 'NONE',  ( -4.000000000000000000, -1.656854249492383024, -1.512499997268811347 ) ) ;
#14026=PLANE ( 'NONE',  #175 ) ;
#14028=CARTESIAN_POINT ( 'NONE',  ( -6.500000000000000888, 1.277696550142688459, -0.05601745114479440152 ) ) ;
#14044=CARTESIAN_POINT ( 'NONE',  ( 1.432654583217642275, -3.458734124999999882, 0.3000000013655960696 ) ) ;
#14074=DIRECTION ( 'NONE',  ( -1.000000000000000000, 0.000000000000000000, 0.000000000000000000 ) ) ;
#14081=CARTESIAN_POINT ( 'NONE',  ( 2.445694354108820079, 2.445694354108820523, -0.3874999986344038194 ) ) ;
#14090=CARTESIAN_POINT ( 'NONE',  ( -2.828427124746189403, -2.828427124746190735, -1.449999997268811347 ) ) ;
#14100=CIRCLE ( 'NONE', #7213, 4.000000000000000000 ) ;
#14103=STYLED_ITEM ( 'NONE', ( #518 ), #8790 ) ;
#14112=CARTESIAN_POINT ( 'NONE',  ( 3.458734125000000326, 4.235727675282971730E-16, 2.237500001365596791 ) ) ;
#14118=CARTESIAN_POINT ( 'NONE',  ( -1.777000578867806491, 3.418741587802790693, 2.039999999999996927 ) ) ;
#14121=CARTESIAN_POINT ( 'NONE',  ( 1.656854249492383024, -3.999999999999999112, -1.387499999999997735 ) ) ;
#14122=VERTEX_POINT ( 'NONE', #20310 ) ;
#14126=ORIENTED_EDGE ( 'NONE', *, *, #9243, .T. ) ;
#14138=( BOUNDED_CURVE ( )  B_SPLINE_CURVE ( 2, ( #6211, #19358, #2480 ),
 .UNSPECIFIED., .F., .F. ) 
 B_SPLINE_CURVE_WITH_KNOTS ( ( 3, 3 ),
 ( 0.9000000000000000222, 0.9098660637381802418 ),
 .UNSPECIFIED. ) 
 CURVE ( )  GEOMETRIC_REPRESENTATION_ITEM ( )  RATIONAL_B_SPLINE_CURVE ( ( 1.000000000000000000, 0.9399192492781022201, 0.9746801811257985726 ) ) 
 REPRESENTATION_ITEM ( '' )  );
#14142=FACE_OUTER_BOUND ( 'NONE', #1055, .T. ) ;
#14144=CARTESIAN_POINT ( 'NONE',  ( -6.500000000000000000, 0.000000000000000000, -3.700000000000000178 ) ) ;
#14146=CARTESIAN_POINT ( 'NONE',  ( 4.000000000000000888, -1.656854249492379694, -2.262499999999998401 ) ) ;
#14148=CARTESIAN_POINT ( 'NONE',  ( -4.000000000000000000, -1.656854249492383024, 0.4875000027311864881 ) ) ;
#14154=CARTESIAN_POINT ( 'NONE',  ( -1.432654583217640276, 3.458734125000000326, -3.449999998634403653 ) ) ;
#14173=EDGE_CURVE ( 'NONE', #12637, #4626, #14873, .T. ) ;
#14174=CARTESIAN_POINT ( 'NONE',  ( -3.458734125000000770, 1.432654583217640498, -2.074999998634404097 ) ) ;
#14192=EDGE_LOOP ( 'NONE', ( #5151, #5445, #6684, #21146, #22183, #12890 ) ) ;
#14203=CARTESIAN_POINT ( 'NONE',  ( -3.381512639161500466, 0.7267833367865139671, -3.295601554149589330 ) ) ;
#14207=CARTESIAN_POINT ( 'NONE',  ( -1.432654583217640498, 3.458734125000000770, 1.800000001365597235 ) ) ;
#14216=CARTESIAN_POINT ( 'NONE',  ( 2.828427124746190735, -2.828427124746189847, -0.1999999972688119854 ) ) ;
#14236=CARTESIAN_POINT ( 'NONE',  ( -3.458734125000000326, 0.000000000000000000, 2.737500001365597235 ) ) ;
#14239=CARTESIAN_POINT ( 'NONE',  ( 4.000000000000000000, 1.656854249492381248, -0.1374999999999984290 ) ) ;
#14256=FACE_OUTER_BOUND ( 'NONE', #21661, .T. ) ;
#14266=DIRECTION ( 'NONE',  ( 0.8660254037844381525, -0.5000000000000006661, 0.000000000000000000 ) ) ;
#14271=ADVANCED_FACE ( 'NONE', ( #1420, #19873 ), #5039, .F. ) ;
#14273=ORIENTED_EDGE ( 'NONE', *, *, #9384, .T. ) ;
#14275=CARTESIAN_POINT ( 'NONE',  ( -1.432654583217640942, -3.458734124999999882, -1.074999998634403209 ) ) ;
#14281=ORIENTED_EDGE ( 'NONE', *, *, #15214, .T. ) ;
#14291=CARTESIAN_POINT ( 'NONE',  ( -2.445694354108819635, -2.445694354108820967, 1.112500001365595681 ) ) ;
#14307=VERTEX_POINT ( 'NONE', #23358 ) ;
#14321=CARTESIAN_POINT ( 'NONE',  ( -3.458734125000000770, 1.432654583217640498, -2.074999998634404097 ) ) ;
#14322=DIRECTION ( 'NONE',  ( 0.000000000000000000, 0.000000000000000000, -1.000000000000000000 ) ) ;
#14329=CARTESIAN_POINT ( 'NONE',  ( 1.656854249492380360, 4.000000000000000000, 1.112500002731187099 ) ) ;
#14335=AXIS2_PLACEMENT_3D ( 'NONE', #23305, #10413, #12434 ) ;
#14339=B_SPLINE_CURVE_WITH_KNOTS ( 'NONE', 3,
 ( #8104, #530, #11817, #15528, #5602, #22676, #15176, #20191 ),
 .UNSPECIFIED., .F., .F.,
 ( 4, 2, 2, 4 ),
 ( 0.003797433802554453681, 0.004743183970586248299, 0.005688934138618042917, 0.007580434474681630418 ),
 .UNSPECIFIED. ) ;
#14347=CARTESIAN_POINT ( 'NONE',  ( 0.000000000000000000, 0.000000000000000000, -3.700000000000000178 ) ) ;
#14352=CARTESIAN_POINT ( 'NONE',  ( 3.458734125000000770, -1.432654583217639610, 3.175000001365598568 ) ) ;
#14365=ORIENTED_EDGE ( 'NONE', *, *, #20736, .F. ) ;
#14382=CARTESIAN_POINT ( 'NONE',  ( -4.714285714285714413, 5.773334910266094008E-16, 3.059999999999998277 ) ) ;
#14392=CARTESIAN_POINT ( 'NONE',  ( 3.458734125000000326, 4.235727675282971730E-16, -2.762499998634404097 ) ) ;
#14408=EDGE_CURVE ( 'NONE', #13238, #7010, #20540, .T. ) ;
#14413=CARTESIAN_POINT ( 'NONE',  ( 1.656854249492380360, 4.000000000000000000, 3.987500000000003375 ) ) ;
#14424=CARTESIAN_POINT ( 'NONE',  ( -3.381512639161500466, 0.7267833367865139671, -3.295601554149589330 ) ) ;
#14448=CARTESIAN_POINT ( 'NONE',  ( 1.656854249492383024, -3.999999999999999112, 0.7375000027311867656 ) ) ;
#14467=CARTESIAN_POINT ( 'NONE',  ( -3.458734125000000326, 0.000000000000000000, -0.2624999986344037084 ) ) ;
#14472=ADVANCED_FACE ( 'NONE', ( #9355 ), #7683, .F. ) ;
#14501=CARTESIAN_POINT ( 'NONE',  ( 3.789206216388694148, -0.2381715126799111015, 2.039999999999999591 ) ) ;
#14537=CARTESIAN_POINT ( 'NONE',  ( 3.458734125000001214, -1.432654583217639610, -2.574999998634404541 ) ) ;
#14550=CARTESIAN_POINT ( 'NONE',  ( -3.458734124999999882, -1.432654583217642275, -3.199999998634404985 ) ) ;
#14576=CARTESIAN_POINT ( 'NONE',  ( -2.828427124746190291, 2.828427124746190291, -3.699999997268811569 ) ) ;
#14578=FACE_OUTER_BOUND ( 'NONE', #21070, .T. ) ;
#14594=CARTESIAN_POINT ( 'NONE',  ( 1.432654583217639832, 3.458734125000000326, -1.574999998634403875 ) ) ;
#14612=DIRECTION ( 'NONE',  ( 0.000000000000000000, 0.000000000000000000, -1.000000000000000000 ) ) ;
#14623=CARTESIAN_POINT ( 'NONE',  ( 4.000000000000000000, 4.898587196589412829E-16, -1.199999999999997957 ) ) ;
#14625=DIRECTION ( 'NONE',  ( 1.000000000000000000, 0.000000000000000000, 0.000000000000000000 ) ) ;
#14631=CARTESIAN_POINT ( 'NONE',  ( -1.432654583217640276, 3.458734125000000326, -0.4499999986344046521 ) ) ;
#14652=CARTESIAN_POINT ( 'NONE',  ( -2.828427124746189403, -2.828427124746190735, 3.425000000000002487 ) ) ;
#14676=CARTESIAN_POINT ( 'NONE',  ( 6.499999999999999112, 0.000000000000000000, 9.480888224575631185 ) ) ;
#14688=CARTESIAN_POINT ( 'NONE',  ( -4.000000000000000000, 0.000000000000000000, -2.574999997268812457 ) ) ;
#14693=CARTESIAN_POINT ( 'NONE',  ( 2.828427124746190735, -2.828427124746189847, -2.324999999999998845 ) ) ;
#14699=CARTESIAN_POINT ( 'NONE',  ( -2.445694354108820523, 2.445694354108820523, 1.862500001365596347 ) ) ;
#14707=CARTESIAN_POINT ( 'NONE',  ( -3.458734125000000326, 0.000000000000000000, 0.7375000013655954589 ) ) ;
#14710=CARTESIAN_POINT ( 'NONE',  ( -1.656854249492380582, 4.000000000000000000, 0.1125000000000017791 ) ) ;
#14722=ORIENTED_EDGE ( 'NONE', *, *, #1603, .F. ) ;
#14734=CARTESIAN_POINT ( 'NONE',  ( 2.697128823393878605, -5.948365447239590154, -3.686277791023379713 ) ) ;
#14736=CARTESIAN_POINT ( 'NONE',  ( -3.250000000000003997, -5.629165124598848102, 1.734723475976807094E-15 ) ) ;
#14737=DIRECTION ( 'NONE',  ( -0.000000000000000000, -0.000000000000000000, 1.000000000000000000 ) ) ;
#14757=CARTESIAN_POINT ( 'NONE',  ( 0.000000000000000000, 0.000000000000000000, -3.700000000000000178 ) ) ;
#14764=CARTESIAN_POINT ( 'NONE',  ( 2.828427124746190735, -2.828427124746189847, -0.1999999972688119854 ) ) ;
#14769=CARTESIAN_POINT ( 'NONE',  ( -2.828427124746190291, 2.828427124746190291, 5.175000000000000711 ) ) ;
#14782=CARTESIAN_POINT ( 'NONE',  ( 4.000000000000000000, 4.898587196589412829E-16, 0.9250000027311873207 ) ) ;
#14789=ADVANCED_FACE ( 'NONE', ( #12618 ), #3702, .F. ) ;
#14805=ORIENTED_EDGE ( 'NONE', *, *, #21184, .T. ) ;
#14807=CARTESIAN_POINT ( 'NONE',  ( -2.117863837641485618E-16, 3.458734125000000326, 5.487500001365596347 ) ) ;
#14809=CARTESIAN_POINT ( 'NONE',  ( 0.2615509004163102946, 3.991439731035835603, 2.039999999999998259 ) ) ;
#14818=CARTESIAN_POINT ( 'NONE',  ( -1.432654583217640498, 3.458734125000000770, -0.1999999986344043745 ) ) ;
#14820=CARTESIAN_POINT ( 'NONE',  ( -2.697128823393878161, 5.948365447239581272, -3.686277791023383710 ) ) ;
#14823=CARTESIAN_POINT ( 'NONE',  ( -2.445694354108819635, -2.445694354108820523, 0.8625000013655955700 ) ) ;
#14853=CARTESIAN_POINT ( 'NONE',  ( 3.349393607134518280, 2.131150051602727302, 2.039999999999998259 ) ) ;
#14867=CARTESIAN_POINT ( 'NONE',  ( -6.500000000000000000, 3.145973671264222116, -0.4053876232513699551 ) ) ;
#14868=EDGE_CURVE ( 'NONE', #7079, #7525, #9873, .T. ) ;
#14873=CIRCLE ( 'NONE', #13700, 4.000000000000000000 ) ;
#14890=CARTESIAN_POINT ( 'NONE',  ( 1.656854249492380360, 4.000000000000000000, 4.987500000000000711 ) ) ;
#14894=PRODUCT_DEFINITION_SHAPE ( 'NONE', 'NONE',  #13574 ) ;
#14917=EDGE_CURVE ( 'NONE', #16269, #4081, #4926, .T. ) ;
#14932=CARTESIAN_POINT ( 'NONE',  ( 1.432654583217642275, -3.458734124999999437, 4.050000001365596347 ) ) ;
#14941=CARTESIAN_POINT ( 'NONE',  ( 6.353591512924457348E-16, -3.458734125000000770, 1.237500001365595903 ) ) ;
#14946=CARTESIAN_POINT ( 'NONE',  ( -2.149058192116894084, 6.264794173742276762, -3.633174458636620141 ) ) ;
#14951=CARTESIAN_POINT ( 'NONE',  ( -2.117863837641485618E-16, 3.458734125000000326, 0.4875000013655952369 ) ) ;
#14961=LINE ( 'NONE', #23555, #13224 ) ;
#14981=CARTESIAN_POINT ( 'NONE',  ( 3.106864633348762617, -1.916927135885768907, 2.039999999999999147 ) ) ;
#14988=CARTESIAN_POINT ( 'NONE',  ( -4.000000000000000000, 4.898587196589412829E-16, 19.04999999999996874 ) ) ;
#15009=EDGE_CURVE ( 'NONE', #11761, #15043, #4253, .T. ) ;
#15015=CARTESIAN_POINT ( 'NONE',  ( 4.000000000000000888, -1.656854249492379694, 2.737500000000002043 ) ) ;
#15042=CARTESIAN_POINT ( 'NONE',  ( 0.000000000000000000, 0.000000000000000000, 9.480888224575631185 ) ) ;
#15043=VERTEX_POINT ( 'NONE', #4125 ) ;
#15046=CARTESIAN_POINT ( 'NONE',  ( -2.445694354108820523, 2.445694354108820523, 5.612500001365596347 ) ) ;
#15058=CARTESIAN_POINT ( 'NONE',  ( -3.458734125000000770, 1.432654583217640498, -0.07499999863440427739 ) ) ;
#15065=CARTESIAN_POINT ( 'NONE',  ( -1.432654583217640276, 3.458734125000000326, -2.449999998634404097 ) ) ;
#15076=EDGE_CURVE ( 'NONE', #6397, #8139, #14339, .T. ) ;
#15080=ORIENTED_EDGE ( 'NONE', *, *, #5123, .T. ) ;
#15082=ORIENTED_EDGE ( 'NONE', *, *, #20606, .F. ) ;
#15115=CARTESIAN_POINT ( 'NONE',  ( 6.500000000000000888, 1.277696550142690457, -3.643982548855206449 ) ) ;
#15118=EDGE_LOOP ( 'NONE', ( #8207, #12541, #1308 ) ) ;
#15126=CARTESIAN_POINT ( 'NONE',  ( -1.656854249492380804, 4.000000000000000000, 0.1125000000000017791 ) ) ;
#15144=EDGE_CURVE ( 'NONE', #669, #21201, #10313, .T. ) ;
#15153=CARTESIAN_POINT ( 'NONE',  ( -1.432654583217641164, -3.458734125000000326, 3.175000001365598568 ) ) ;
#15163=CARTESIAN_POINT ( 'NONE',  ( -3.458734125000000326, 1.432654583217640276, 2.675000001365597679 ) ) ;
#15175=CARTESIAN_POINT ( 'NONE',  ( 3.458734125000000770, 4.235727675282972223E-16, -1.512499998634402987 ) ) ;
#15176=CARTESIAN_POINT ( 'NONE',  ( -5.969670414742686226, -4.058962678540103397, -3.296219944818621350 ) ) ;
#15181=CARTESIAN_POINT ( 'NONE',  ( 6.353591512924457348E-16, -3.458734125000000326, -2.012499998634403653 ) ) ;
#15188=CARTESIAN_POINT ( 'NONE',  ( -1.656854249492380804, 4.000000000000000000, 4.237500002731185766 ) ) ;
#15203=CARTESIAN_POINT ( 'NONE',  ( 0.000000000000000000, 0.000000000000000000, -3.700000000000000178 ) ) ;
#15214=EDGE_CURVE ( 'NONE', #2635, #10924, #1226, .T. ) ;
#15222=CARTESIAN_POINT ( 'NONE',  ( 1.656854249492380138, 4.000000000000000000, 0.9875000000000007105 ) ) ;
#15237=DIRECTION ( 'NONE',  ( 1.000000000000000000, 0.000000000000000000, 0.000000000000000000 ) ) ;
#15242=CARTESIAN_POINT ( 'NONE',  ( -1.656854249492380804, 4.000000000000000000, 2.112500000000001599 ) ) ;
#15256=VERTEX_POINT ( 'NONE', #16107 ) ;
#15266=( BOUNDED_CURVE ( )  B_SPLINE_CURVE ( 2, ( #13291, #6083, #10826, #330, #18101, #22353, #4287, #1681, #9025 ),
 .UNSPECIFIED., .F., .F. ) 
 B_SPLINE_CURVE_WITH_KNOTS ( ( 3, 2, 2, 2, 3 ),
 ( 0.5500000000000000444, 0.5625000000000000000, 0.5749999999999999556, 0.5875000000000000222, 0.5999999999999999778 ),
 .UNSPECIFIED. ) 
 CURVE ( )  GEOMETRIC_REPRESENTATION_ITEM ( )  RATIONAL_B_SPLINE_CURVE ( ( 1.000000000000000000, 0.9238795325112867385, 1.000000000000000000, 0.9238795325112867385, 1.000000000000000000, 0.9238795325112867385, 1.000000000000000000, 0.9238795325112867385, 1.000000000000000000 ) ) 
 REPRESENTATION_ITEM ( '' )  );
#15271=AXIS2_PLACEMENT_3D ( 'NONE', #18631, #2217, #16852 ) ;
#15272=CARTESIAN_POINT ( 'NONE',  ( 2.445694354108820079, 2.445694354108820523, 4.612500001365595459 ) ) ;
#15281=CARTESIAN_POINT ( 'NONE',  ( -2.445694354108819635, -2.445694354108820523, 1.862500001365596347 ) ) ;
#15283=CARTESIAN_POINT ( 'NONE',  ( -3.458734124999999882, -1.432654583217642275, -0.1999999986344043745 ) ) ;
#15303=CARTESIAN_POINT ( 'NONE',  ( -3.458734125000000770, 0.000000000000000000, 3.987500001365595015 ) ) ;
#15313=CARTESIAN_POINT ( 'NONE',  ( -2.449293598294706907E-16, 4.000000000000000000, 3.175000002731189319 ) ) ;
#15323=VECTOR ( 'NONE', #9424, 1000.000000000000000 ) ;
#15324=UNCERTAINTY_MEASURE_WITH_UNIT (LENGTH_MEASURE( 1.000000000000000082E-05 ), #9885, 'distance_accuracy_value', 'NONE');
#15328=ORIENTED_EDGE ( 'NONE', *, *, #11754, .F. ) ;
#15336=ORIENTED_EDGE ( 'NONE', *, *, #12738, .F. ) ;
#15358=ORIENTED_EDGE ( 'NONE', *, *, #10108, .F. ) ;
#15360=CARTESIAN_POINT ( 'NONE',  ( 3.802871176606126280, 5.309964801958118485, -0.01372220897661548429 ) ) ;
#15366=EDGE_LOOP ( 'NONE', ( #757, #5631 ) ) ;
#15367=CARTESIAN_POINT ( 'NONE',  ( 7.347880794884118750E-16, -4.000000000000000000, 0.5500000000000018208 ) ) ;
#15393=CARTESIAN_POINT ( 'NONE',  ( -2.445694354108819635, -2.445694354108820967, 4.112500001365594571 ) ) ;
#15402=CARTESIAN_POINT ( 'NONE',  ( -1.432654583217640276, 3.458734125000000326, 0.5500000013655963471 ) ) ;
#15404=CARTESIAN_POINT ( 'NONE',  ( 6.353591512924457348E-16, -3.458734125000000326, 0.9875000013655956810 ) ) ;
#15405=VERTEX_POINT ( 'NONE', #7803 ) ;
#15413=CARTESIAN_POINT ( 'NONE',  ( -2.117863837641485618E-16, 3.458734125000000770, -3.262499998634402765 ) ) ;
#15414=EDGE_CURVE ( 'NONE', #21201, #6989, #1422, .T. ) ;
#15421=CARTESIAN_POINT ( 'NONE',  ( 6.353591512924457348E-16, -3.458734125000000326, -3.012499998634404541 ) ) ;
#15427=CARTESIAN_POINT ( 'NONE',  ( 4.000000000000000000, 1.656854249492381248, -2.137499999999998401 ) ) ;
#15442=ORIENTED_EDGE ( 'NONE', *, *, #9490, .F. ) ;
#15461=CARTESIAN_POINT ( 'NONE',  ( 5.969670414742682674, 4.058962678540098956, -3.296219944818626235 ) ) ;
#15471=CARTESIAN_POINT ( 'NONE',  ( 3.525817189091411397, 5.469921996229798467, 4.860839739976680053E-15 ) ) ;
#15479=CARTESIAN_POINT ( 'NONE',  ( -4.000000000000000000, -1.656854249492383246, 0.3625000000000019873 ) ) ;
#15491=ORIENTED_EDGE ( 'NONE', *, *, #137, .F. ) ;
#15504=CARTESIAN_POINT ( 'NONE',  ( -1.432654583217640498, 3.458734125000000770, 1.800000001365597235 ) ) ;
#15509=EDGE_LOOP ( 'NONE', ( #837, #12576, #9290, #2221 ) ) ;
#15511=VERTEX_POINT ( 'NONE', #6230 ) ;
#15514=CARTESIAN_POINT ( 'NONE',  ( 1.432654583217642275, -3.458734124999999437, 0.05000000136559582670 ) ) ;
#15516=CARTESIAN_POINT ( 'NONE',  ( 3.458734125000000326, 1.432654583217640498, -0.6999999986344048741 ) ) ;
#15528=CARTESIAN_POINT ( 'NONE',  ( -4.350941807883113910, -4.993536075455430101, -3.633174458636617921 ) ) ;
#15539=CARTESIAN_POINT ( 'NONE',  ( -2.117863837641485618E-16, 3.458734125000000326, -2.512499998634404097 ) ) ;
#15547=CARTESIAN_POINT ( 'NONE',  ( 4.000000000000000888, -1.656854249492379694, 2.862500002731188431 ) ) ;
#15570=DIRECTION ( 'NONE',  ( 1.000000000000000000, 0.000000000000000000, 0.000000000000000000 ) ) ;
#15583=CARTESIAN_POINT ( 'NONE',  ( 3.525817189091411841, 5.469921996229796690, -3.700000000000005063 ) ) ;
#15592=CARTESIAN_POINT ( 'NONE',  ( 0.000000000000000000, 0.000000000000000000, 19.04999999999996874 ) ) ;
#15610=DIRECTION ( 'NONE',  ( -0.000000000000000000, -0.000000000000000000, 1.000000000000000000 ) ) ;
#15624=VECTOR ( 'NONE', #2848, 1000.000000000000000 ) ;
#15625=CARTESIAN_POINT ( 'NONE',  ( 2.445694354108820967, -2.445694354108820079, 3.362500001365597679 ) ) ;
#15635=CARTESIAN_POINT ( 'NONE',  ( -3.458734125000000326, 1.432654583217640276, -1.324999998634403209 ) ) ;
#15644=CARTESIAN_POINT ( 'NONE',  ( -2.445694354108820523, 2.445694354108820523, -1.137499998634402765 ) ) ;
#15647=DIRECTION ( 'NONE',  ( -0.000000000000000000, -0.000000000000000000, 1.000000000000000000 ) ) ;
#15650=EDGE_CURVE ( 'NONE', #21452, #19427, #11996, .T. ) ;
#15655=CARTESIAN_POINT ( 'NONE',  ( 2.445694354108820079, 2.445694354108820523, 0.6125000013655953479 ) ) ;
#15664=CARTESIAN_POINT ( 'NONE',  ( -4.000000000000000000, -1.656854249492383246, 2.487500002731188431 ) ) ;
#15667=CARTESIAN_POINT ( 'NONE',  ( 4.000000000000000000, 4.898587196589412829E-16, 1.925000002731188209 ) ) ;
#15683=CARTESIAN_POINT ( 'NONE',  ( 2.445694354108820079, 2.445694354108820523, 3.362500001365597679 ) ) ;
#15704=CARTESIAN_POINT ( 'NONE',  ( -5.968343123267132455, 4.059728990630802059, -0.4033376246892508288 ) ) ;
#15721=CARTESIAN_POINT ( 'NONE',  ( -2.828427124746189403, -2.828427124746190735, -2.574999999999999289 ) ) ;
#15724=DIRECTION ( 'NONE',  ( -1.000000000000000000, 0.000000000000000000, 0.000000000000000000 ) ) ;
#15738=AXIS2_PLACEMENT_3D ( 'NONE', #17144, #7926, #15724 ) ;
#15745=CARTESIAN_POINT ( 'NONE',  ( 6.353591512924457348E-16, -3.458734125000000770, 0.2375000013655967357 ) ) ;
#15754=DIRECTION ( 'NONE',  ( -1.000000000000000000, 0.000000000000000000, 0.000000000000000000 ) ) ;
#15758=VERTEX_POINT ( 'NONE', #7184 ) ;
#15763=CARTESIAN_POINT ( 'NONE',  ( -3.381512639161500466, 0.7267833367865139671, -3.295601554149589330 ) ) ;
#15770=CARTESIAN_POINT ( 'NONE',  ( 2.445694354108820079, 2.445694354108820523, 2.612500001365597235 ) ) ;
#15778=ORIENTED_EDGE ( 'NONE', *, *, #16405, .F. ) ;
#15780=CARTESIAN_POINT ( 'NONE',  ( -1.656854249492381248, -3.999999999999999112, 1.612500002731187543 ) ) ;
#15794=CARTESIAN_POINT ( 'NONE',  ( 1.432654583217639832, 3.458734125000000326, 2.425000001365597679 ) ) ;
#15816=VERTEX_POINT ( 'NONE', #3678 ) ;
#15819=CARTESIAN_POINT ( 'NONE',  ( 7.347880794884118750E-16, -4.000000000000000000, -1.324999997268811347 ) ) ;
#15825=CARTESIAN_POINT ( 'NONE',  ( 4.000000000000000888, -1.656854249492379694, -1.262499999999997513 ) ) ;
#15833=CARTESIAN_POINT ( 'NONE',  ( -6.500000000000000000, 0.6345343291280529652, 5.374424050328533679E-16 ) ) ;
#15835=EDGE_CURVE ( 'NONE', #21232, #6397, #20993, .T. ) ;
#15850=CARTESIAN_POINT ( 'NONE',  ( 3.458734125000000770, 1.432654583217640498, -0.4499999986344046521 ) ) ;
#15864=DIRECTION ( 'NONE',  ( -1.000000000000000000, 1.224646799147353207E-16, 0.000000000000000000 ) ) ;
#15868=ORIENTED_EDGE ( 'NONE', *, *, #10108, .T. ) ;
#15878=CARTESIAN_POINT ( 'NONE',  ( -3.458734125000000770, 1.432654583217640498, 1.925000001365597457 ) ) ;
#15886=CARTESIAN_POINT ( 'NONE',  ( 1.656854249492383024, -3.999999999999999112, -0.2624999972688122352 ) ) ;
#15900=DIRECTION ( 'NONE',  ( 0.000000000000000000, 0.000000000000000000, 1.000000000000000000 ) ) ;
#15903=CARTESIAN_POINT ( 'NONE',  ( -1.432654583217640276, 3.458734125000000326, 4.550000001365596347 ) ) ;
#15908=CARTESIAN_POINT ( 'NONE',  ( -3.202817526797028247, 1.848609732162391772, 2.039999999999998259 ) ) ;
#15916=DIRECTION ( 'NONE',  ( 1.000000000000000000, 0.000000000000000000, 0.000000000000000000 ) ) ;
#15928=ADVANCED_FACE ( 'NONE', ( #11506 ), #16987, .F. ) ;
#15932=CARTESIAN_POINT ( 'NONE',  ( -6.500000000000000888, -2.517290933526015628, -3.443420074781601947 ) ) ;
#15934=CARTESIAN_POINT ( 'NONE',  ( -1.656854249492381248, -3.999999999999999112, -1.512499999999997735 ) ) ;
#15937=CARTESIAN_POINT ( 'NONE',  ( 4.350525068611871049, -4.993776679985862721, -0.05533025579362501473 ) ) ;
#15938=CARTESIAN_POINT ( 'NONE',  ( -2.445694354108819635, -2.445694354108820523, -0.1374999986344035974 ) ) ;
#15958=CARTESIAN_POINT ( 'NONE',  ( 3.458734125000000770, 4.235727675282972223E-16, -1.512499998634402987 ) ) ;
#15990=EDGE_CURVE ( 'NONE', #10158, #2314, #12190, .T. ) ;
#15992=CARTESIAN_POINT ( 'NONE',  ( 3.458734125000000770, 1.432654583217640498, 1.550000001365597013 ) ) ;
#15993=CARTESIAN_POINT ( 'NONE',  ( 0.000000000000000000, 0.000000000000000000, 0.000000000000000000 ) ) ;
#16001=CARTESIAN_POINT ( 'NONE',  ( -2.828427124746190291, 2.828427124746190291, 1.300000002731187543 ) ) ;
#16010=COLOUR_RGB ( '', 0.31764706, 0.68627451, 0.89019608) ;
#16020=CARTESIAN_POINT ( 'NONE',  ( 6.353591512924457348E-16, -3.458734125000000326, 4.987500001365595459 ) ) ;
#16027=CARTESIAN_POINT ( 'NONE',  ( -2.031236510114588611, 3.247785564556652460, 2.039999999999996927 ) ) ;
#16054=FACE_OUTER_BOUND ( 'NONE', #14192, .T. ) ;
#16060=EDGE_CURVE ( 'NONE', #18029, #10634, #4948, .T. ) ;
#16062=CARTESIAN_POINT ( 'NONE',  ( -3.458734125000000326, 0.000000000000000000, -1.262499998634402765 ) ) ;
#16080=FACE_OUTER_BOUND ( 'NONE', #1512, .T. ) ;
#16082=CARTESIAN_POINT ( 'NONE',  ( 6.353591512924457348E-16, -3.458734125000000770, -1.762499998634403209 ) ) ;
#16095=CARTESIAN_POINT ( 'NONE',  ( -1.432654583217640942, -3.458734124999999882, -2.074999998634404097 ) ) ;
#16106=CARTESIAN_POINT ( 'NONE',  ( -3.416564614606786066, 1.811858101813906607, -3.557290855993161305 ) ) ;
#16107=CARTESIAN_POINT ( 'NONE',  ( 4.714285714285714413, 0.000000000000000000, 3.059999999999998277 ) ) ;
#16112=DIRECTION ( 'NONE',  ( -0.000000000000000000, -0.000000000000000000, 1.000000000000000000 ) ) ;
#16114=CARTESIAN_POINT ( 'NONE',  ( 3.458734125000000770, 1.432654583217640498, 3.550000001365598568 ) ) ;
#16115=CARTESIAN_POINT ( 'NONE',  ( -3.270501301980698550, -1.125461230421587633, 2.040000000000001812 ) ) ;
#16123=CARTESIAN_POINT ( 'NONE',  ( -4.000000000000000000, -1.656854249492383246, -0.5124999972688124572 ) ) ;
#16128=ORIENTED_EDGE ( 'NONE', *, *, #247, .F. ) ;
#16142=CARTESIAN_POINT ( 'NONE',  ( -3.458734125000000326, 1.432654583217640276, 4.675000001365594571 ) ) ;
#16149=CARTESIAN_POINT ( 'NONE',  ( 4.000000000000000888, -1.656854249492379694, -1.262499999999997513 ) ) ;
#16162=( BOUNDED_CURVE ( )  B_SPLINE_CURVE ( 2, ( #13505, #22933, #2921, #23048, #9785, #21118, #10271, #15427, #4262 ),
 .UNSPECIFIED., .F., .F. ) 
 B_SPLINE_CURVE_WITH_KNOTS ( ( 3, 2, 2, 2, 3 ),
 ( 0.8000000000000000444, 0.8125000000000000000, 0.8249999999999999556, 0.8375000000000000222, 0.8499999999999999778 ),
 .UNSPECIFIED. ) 
 CURVE ( )  GEOMETRIC_REPRESENTATION_ITEM ( )  RATIONAL_B_SPLINE_CURVE ( ( 1.000000000000000000, 0.9238795325112867385, 1.000000000000000000, 0.9238795325112867385, 1.000000000000000000, 0.9238795325112867385, 1.000000000000000000, 0.9238795325112867385, 1.000000000000000000 ) ) 
 REPRESENTATION_ITEM ( '' )  );
#16171=CARTESIAN_POINT ( 'NONE',  ( -6.500000000000000000, -0.6341575537611434665, -3.700000000000001066 ) ) ;
#16179=CARTESIAN_POINT ( 'NONE',  ( 3.458734125000000326, 1.432654583217640498, -1.699999998634404097 ) ) ;
#16188=DIRECTION ( 'NONE',  ( 1.000000000000000000, 0.000000000000000000, 0.000000000000000000 ) ) ;
#16193=CYLINDRICAL_SURFACE ( 'NONE', #8395, 6.499999999999999112 ) ;
#16197=CARTESIAN_POINT ( 'NONE',  ( 2.828427124746189847, 2.828427124746190291, 5.925000000000001599 ) ) ;
#16232=ORIENTED_EDGE ( 'NONE', *, *, #15009, .F. ) ;
#16234=CARTESIAN_POINT ( 'NONE',  ( 2.828427124746189847, 2.828427124746190291, 0.05000000273118650196 ) ) ;
#16246=DIRECTION ( 'NONE',  ( -0.000000000000000000, -0.000000000000000000, 1.000000000000000000 ) ) ;
#16249=EDGE_CURVE ( 'NONE', #4081, #16269, #11882, .T. ) ;
#16255=CARTESIAN_POINT ( 'NONE',  ( 3.458734125000000326, 4.235727675282971730E-16, 0.2375000013655967357 ) ) ;
#16269=VERTEX_POINT ( 'NONE', #8962 ) ;
#16272=CARTESIAN_POINT ( 'NONE',  ( 0.000000000000000000, 0.000000000000000000, 3.059999999999998277 ) ) ;
#16285=CARTESIAN_POINT ( 'NONE',  ( 1.709085384558223675, -3.079427455697027138, 2.039999999999996927 ) ) ;
#16289=CIRCLE ( 'NONE', #3645, 5.479999999999998650 ) ;
#16295=CARTESIAN_POINT ( 'NONE',  ( 4.000000000000000000, 4.898587196589412829E-16, 0.9250000027311873207 ) ) ;
#16299=CARTESIAN_POINT ( 'NONE',  ( -2.117863837641485618E-16, 3.458734125000000326, -3.512499998634403209 ) ) ;
#16303=ORIENTED_EDGE ( 'NONE', *, *, #17898, .T. ) ;
#16309=DIRECTION ( 'NONE',  ( -1.000000000000000000, -3.552713678800500929E-15, 0.000000000000000000 ) ) ;
#16310=DIRECTION ( 'NONE',  ( 1.000000000000000000, 0.000000000000000000, 0.000000000000000000 ) ) ;
#16316=CYLINDRICAL_SURFACE ( 'NONE', #18744, 4.000000000000000000 ) ;
#16317=CARTESIAN_POINT ( 'NONE',  ( 2.828427124746189847, 2.828427124746190291, 3.925000000000002931 ) ) ;
#16327=CARTESIAN_POINT ( 'NONE',  ( -3.458734125000000326, 0.000000000000000000, -2.262499998634403653 ) ) ;
#16349=CARTESIAN_POINT ( 'NONE',  ( 7.347880794884118750E-16, -4.000000000000000000, -2.324999997268812013 ) ) ;
#16355=CARTESIAN_POINT ( 'NONE',  ( -1.647987302177966740E-14, -7.505553499465137612, -0.5805565836007695601 ) ) ;
#16368=CARTESIAN_POINT ( 'NONE',  ( -1.432654583217640942, -3.458734124999999882, -0.07499999863440427739 ) ) ;
#16370=CARTESIAN_POINT ( 'NONE',  ( 2.828427124746189847, 2.828427124746190291, -0.07499999999999867883 ) ) ;
#16374=CARTESIAN_POINT ( 'NONE',  ( 6.499999999999999112, -1.264206540070616835, -3.645490429492275197 ) ) ;
#16379=ORIENTED_EDGE ( 'NONE', *, *, #12738, .T. ) ;
#16392=CARTESIAN_POINT ( 'NONE',  ( 4.000000000000000888, -1.656854249492379694, -0.2624999999999966804 ) ) ;
#16398=CARTESIAN_POINT ( 'NONE',  ( 3.596871450741750742, 1.575092265385753310, 2.039999999999997815 ) ) ;
#16403=PLANE ( 'NONE',  #3948 ) ;
#16405=EDGE_CURVE ( 'NONE', #11298, #20452, #6916, .T. ) ;
#16412=LINE ( 'NONE', #12950, #10167 ) ;
#16432=CARTESIAN_POINT ( 'NONE',  ( -4.000000000000000000, 0.000000000000000000, 6.300000000000001599 ) ) ;
#16470=CARTESIAN_POINT ( 'NONE',  ( 4.000000000000000000, 1.656854249492381248, -3.012499997268812457 ) ) ;
#16477=CARTESIAN_POINT ( 'NONE',  ( 1.125461230421587633, -3.270501301980698550, 2.040000000000001812 ) ) ;
#16478=CARTESIAN_POINT ( 'NONE',  ( 2.445694354108820967, -2.445694354108820079, -0.6374999986344023206 ) ) ;
#16487=CARTESIAN_POINT ( 'NONE',  ( 2.445694354108820079, 2.445694354108820523, 1.362500001365595903 ) ) ;
#16493=CARTESIAN_POINT ( 'NONE',  ( -0.04760896646565748735, 3.990996980104895897, 2.039999999999998259 ) ) ;
#16497=ORIENTED_EDGE ( 'NONE', *, *, #9490, .T. ) ;
#16535=CARTESIAN_POINT ( 'NONE',  ( 6.500000000000000000, 3.752776749732563477, -3.700000000000000178 ) ) ;
#16543=CARTESIAN_POINT ( 'NONE',  ( 4.000000000000000000, 4.898587196589412829E-16, -0.07499999726881187434 ) ) ;
#16547=CARTESIAN_POINT ( 'NONE',  ( 7.347880794884118750E-16, -4.000000000000000000, 5.550000000000000711 ) ) ;
#16558=CARTESIAN_POINT ( 'NONE',  ( -2.449293598294706907E-16, 4.000000000000000000, -2.949999999999997957 ) ) ;
#16582=CARTESIAN_POINT ( 'NONE',  ( 3.458734125000000326, 1.432654583217640498, 4.300000001365595459 ) ) ;
#16583=CARTESIAN_POINT ( 'NONE',  ( -4.350941807883110357, -4.993536075455427437, -0.06682554136338243744 ) ) ;
#16584=ORIENTED_EDGE ( 'NONE', *, *, #13815, .T. ) ;
#16593=CARTESIAN_POINT ( 'NONE',  ( 6.353591512924457348E-16, -3.458734125000000770, -0.7624999986344024316 ) ) ;
#16599=CARTESIAN_POINT ( 'NONE',  ( 2.445694354108820523, -2.445694354108820079, 1.112500001365595681 ) ) ;
#16601=EDGE_CURVE ( 'NONE', #19016, #12637, #11224, .T. ) ;
#16631=ORIENTED_EDGE ( 'NONE', *, *, #3538, .T. ) ;
#16632=CARTESIAN_POINT ( 'NONE',  ( -3.250000000000003997, -5.629165124598848102, 1.734723475976807094E-15 ) ) ;
#16657=CARTESIAN_POINT ( 'NONE',  ( -4.000000000000000000, -1.656854249492383024, -0.5124999972688124572 ) ) ;
#16661=CARTESIAN_POINT ( 'NONE',  ( 6.353591512924457348E-16, -3.458734125000000770, -2.762499998634404097 ) ) ;
#16662=CARTESIAN_POINT ( 'NONE',  ( -1.656854249492380804, 4.000000000000000000, 5.112500000000002487 ) ) ;
#16698=CARTESIAN_POINT ( 'NONE',  ( -3.458734125000000326, 0.000000000000000000, 4.737500001365595459 ) ) ;
#16709=CARTESIAN_POINT ( 'NONE',  ( -3.458734125000000326, -0.5784715375562745621, 2.012736001390157181 ) ) ;
#16715=CARTESIAN_POINT ( 'NONE',  ( 2.445694354108820079, 2.445694354108820523, 0.3625000013655951259 ) ) ;
#16730=ORIENTED_EDGE ( 'NONE', *, *, #9423, .T. ) ;
#16734=VECTOR ( 'NONE', #1580, 1000.000000000000000 ) ;
#16744=CARTESIAN_POINT ( 'NONE',  ( -4.000000000000000888, 1.656854249492380582, 0.3625000027311864881 ) ) ;
#16752=CARTESIAN_POINT ( 'NONE',  ( 5.968343123267133343, -4.059728990630809164, -3.296662375310746906 ) ) ;
#16784=CARTESIAN_POINT ( 'NONE',  ( -4.000000000000000000, 0.000000000000000000, 1.300000000000000711 ) ) ;
#16799=EDGE_LOOP ( 'NONE', ( #6868, #5797, #23494, #16730 ) ) ;
#16806=CARTESIAN_POINT ( 'NONE',  ( -0.9709838737629333805, 3.325368937167130223, -3.295601554149325541 ) ) ;
#16812=LINE ( 'NONE', #7831, #2787 ) ;
#16813=ADVANCED_FACE ( 'NONE', ( #3039 ), #16316, .F. ) ;
#16826=CARTESIAN_POINT ( 'NONE',  ( 1.656854249492383024, -3.999999999999999112, -2.262499997268812013 ) ) ;
#16828=CARTESIAN_POINT ( 'NONE',  ( -4.623144047065557594, -4.836380039389424290, -0.1061556211655376447 ) ) ;
#16835=CARTESIAN_POINT ( 'NONE',  ( 3.458734125000000770, 4.235727675282972223E-16, 1.487500001365596125 ) ) ;
#16837=AXIS2_PLACEMENT_3D ( 'NONE', #6562, #21136, #4749 ) ;
#16845=CARTESIAN_POINT ( 'NONE',  ( 3.458734125000000770, 1.432654583217640498, 4.550000001365596347 ) ) ;
#16852=DIRECTION ( 'NONE',  ( -1.000000000000000000, 0.000000000000000000, 0.000000000000000000 ) ) ;
#16858=ORIENTED_EDGE ( 'NONE', *, *, #5092, .F. ) ;
#16860=DIRECTION ( 'NONE',  ( -0.000000000000000000, -0.000000000000000000, 1.000000000000000000 ) ) ;
#16872=DIRECTION ( 'NONE',  ( 1.000000000000000000, 0.000000000000000000, 0.000000000000000000 ) ) ;
#16879=CARTESIAN_POINT ( 'NONE',  ( 3.250000000000002665, -5.629165124598850767, -3.700000000000000178 ) ) ;
#16895=CARTESIAN_POINT ( 'NONE',  ( 4.000000000000000888, -1.656854249492379694, 1.737500000000001377 ) ) ;
#16897=CARTESIAN_POINT ( 'NONE',  ( -3.250000000000004441, 5.629165124598849879, -3.700000000000000178 ) ) ;
#16902=CARTESIAN_POINT ( 'NONE',  ( 4.623144047065553153, 4.836380039389420737, -0.1061556211655326765 ) ) ;
#16907=CARTESIAN_POINT ( 'NONE',  ( 3.458734125000000770, 1.432654583217640498, -0.4499999986344046521 ) ) ;
#16908=CARTESIAN_POINT ( 'NONE',  ( -4.000000000000000888, 1.656854249492380804, 1.237500000000000933 ) ) ;
#16933=CARTESIAN_POINT ( 'NONE',  ( -3.458734125000000770, 0.000000000000000000, 3.987500001365595015 ) ) ;
#16941=( NAMED_UNIT ( * ) PLANE_ANGLE_UNIT ( ) SI_UNIT ( $, .RADIAN. ) );
#16942=CARTESIAN_POINT ( 'NONE',  ( -2.445694354108820523, 2.445694354108820523, 2.612500001365597235 ) ) ;
#16958=CARTESIAN_POINT ( 'NONE',  ( 6.353591512924457348E-16, -3.458734125000000770, 4.237500001365595459 ) ) ;
#16987=CYLINDRICAL_SURFACE ( 'NONE', #20610, 4.000000000000000000 ) ;
#16994=CARTESIAN_POINT ( 'NONE',  ( -6.500000000000000000, 3.752776749732573247, -3.119443416399232394 ) ) ;
#17014=EDGE_CURVE ( 'NONE', #21452, #5142, #556, .T. ) ;
#17022=CARTESIAN_POINT ( 'NONE',  ( 2.828427124746190735, -2.828427124746189847, -0.3249999999999971800 ) ) ;
#17023=CARTESIAN_POINT ( 'NONE',  ( -2.828427124746189403, -2.828427124746190735, -3.449999997268813345 ) ) ;
#17033=ORIENTED_EDGE ( 'NONE', *, *, #5266, .F. ) ;
#17049=CARTESIAN_POINT ( 'NONE',  ( -1.432654583217641164, -3.458734125000000326, 4.175000001365593683 ) ) ;
#17058=( NAMED_UNIT ( * ) SI_UNIT ( $, .STERADIAN. ) SOLID_ANGLE_UNIT ( ) );
#17059=CARTESIAN_POINT ( 'NONE',  ( 1.432654583217639832, 3.458734125000000326, 0.4250000013655961251 ) ) ;
#17061=CARTESIAN_POINT ( 'NONE',  ( 6.353591512924457348E-16, -3.458734125000000326, -0.01249999863440348635 ) ) ;
#17069=CARTESIAN_POINT ( 'NONE',  ( -3.458734125000000770, 0.000000000000000000, -2.012499998634403653 ) ) ;
#17076=CARTESIAN_POINT ( 'NONE',  ( -2.445694354108820523, 2.445694354108820523, -2.387499998634403653 ) ) ;
#17084=CARTESIAN_POINT ( 'NONE',  ( 4.000000000000000000, 4.898587196589412829E-16, 3.925000002731186655 ) ) ;
#17111=AXIS2_PLACEMENT_3D ( 'NONE', #13534, #17356, #2726 ) ;
#17126=CARTESIAN_POINT ( 'NONE',  ( 6.500000000000000888, 0.000000000000000000, -3.700000000000000178 ) ) ;
#17140=CARTESIAN_POINT ( 'NONE',  ( -4.000000000000000000, -1.656854249492383246, 1.362500000000001155 ) ) ;
#17144=CARTESIAN_POINT ( 'NONE',  ( 0.000000000000000000, 0.000000000000000000, -3.700000000000000178 ) ) ;
#17169=CARTESIAN_POINT ( 'NONE',  ( -2.117863837641485618E-16, 3.458734125000000770, 3.737500001365594571 ) ) ;
#17178=CARTESIAN_POINT ( 'NONE',  ( 3.458734125000000770, -1.432654583217639610, 1.175000001365597013 ) ) ;
#17181=CARTESIAN_POINT ( 'NONE',  ( 1.432654583217642053, -3.458734124999999437, 1.050000001365596791 ) ) ;
#17195=AXIS2_PLACEMENT_3D ( 'NONE', #2496, #11645, #18801 ) ;
#17201=CARTESIAN_POINT ( 'NONE',  ( 3.458734125000001214, -1.432654583217639610, 5.425000001365595459 ) ) ;
#17211=CARTESIAN_POINT ( 'NONE',  ( 4.000000000000000888, -1.656854249492379694, 3.862500002731187543 ) ) ;
#17252=DIRECTION ( 'NONE',  ( -0.000000000000000000, -0.000000000000000000, 1.000000000000000000 ) ) ;
#17266=CARTESIAN_POINT ( 'NONE',  ( 4.000000000000000000, 4.898587196589412829E-16, 1.800000000000001155 ) ) ;
#17292=CARTESIAN_POINT ( 'NONE',  ( 3.458734125000000770, 4.235727675282972223E-16, 4.487500001365595459 ) ) ;
#17301=CARTESIAN_POINT ( 'NONE',  ( -3.458734124999999882, -1.432654583217642497, 0.8000000013655964581 ) ) ;
#17302=CARTESIAN_POINT ( 'NONE',  ( 2.445694354108820523, -2.445694354108820079, 1.112500001365595681 ) ) ;
#17311=CARTESIAN_POINT ( 'NONE',  ( 1.432654583217642053, -3.458734124999999882, -2.699999998634404541 ) ) ;
#17314=DIRECTION ( 'NONE',  ( -0.000000000000000000, -0.000000000000000000, 1.000000000000000000 ) ) ;
#17320=CARTESIAN_POINT ( 'NONE',  ( 3.458734125000000770, 1.432654583217640498, 5.550000001365596347 ) ) ;
#17330=CARTESIAN_POINT ( 'NONE',  ( -4.000000000000000000, -1.656854249492383246, 4.487500002731186655 ) ) ;
#17348=FACE_OUTER_BOUND ( 'NONE', #21838, .T. ) ;
#17353=ORIENTED_EDGE ( 'NONE', *, *, #5266, .T. ) ;
#17356=DIRECTION ( 'NONE',  ( 0.000000000000000000, -0.000000000000000000, 1.000000000000000000 ) ) ;
#17361=CARTESIAN_POINT ( 'NONE',  ( 6.500000000000000000, 3.752776749732573247, -3.119443416399232394 ) ) ;
#17365=DIRECTION ( 'NONE',  ( 1.000000000000000000, 0.000000000000000000, 0.000000000000000000 ) ) ;
#17373=B_SPLINE_CURVE_WITH_KNOTS ( 'NONE', 3,
 ( #10379, #16106, #113, #15763 ),
 .UNSPECIFIED., .F., .F.,
 ( 4, 4 ),
 ( 8.673617379884032583E-19, 0.001664000150434504811 ),
 .UNSPECIFIED. ) ;
#17377=CARTESIAN_POINT ( 'NONE',  ( -4.000000000000000888, 1.656854249492380804, -2.762499999999997069 ) ) ;
#17383=ADVANCED_FACE ( 'NONE', ( #14142 ), #4770, .T. ) ;
#17385=ORIENTED_EDGE ( 'NONE', *, *, #11094, .T. ) ;
#17405=CARTESIAN_POINT ( 'NONE',  ( -2.445694354108819635, -2.445694354108820967, 5.112500001365595459 ) ) ;
#17415=CARTESIAN_POINT ( 'NONE',  ( 2.445694354108820079, 2.445694354108820523, 2.362500001365596791 ) ) ;
#17417=CARTESIAN_POINT ( 'NONE',  ( -3.458734124999999882, -1.432654583217642275, -1.199999998634403209 ) ) ;
#17420=CYLINDRICAL_SURFACE ( 'NONE', #22881, 4.000000000000000000 ) ;
#17425=EDGE_CURVE ( 'NONE', #10489, #844, #6123, .T. ) ;
#17429=CARTESIAN_POINT ( 'NONE',  ( -2.445694354108820523, 2.445694354108820523, -2.137499998634403653 ) ) ;
#17440=CARTESIAN_POINT ( 'NONE',  ( -3.458734125000000770, 1.432654583217640498, 0.9250000013655964581 ) ) ;
#17449=CARTESIAN_POINT ( 'NONE',  ( -2.828427124746189403, -2.828427124746190735, 4.550000002731186655 ) ) ;
#17457=EDGE_LOOP ( 'NONE', ( #10282, #16303, #12574, #4302 ) ) ;
#17466=CARTESIAN_POINT ( 'NONE',  ( 3.458734125000000326, 1.432654583217640498, 5.300000001365596347 ) ) ;
#17479=ORIENTED_EDGE ( 'NONE', *, *, #18128, .T. ) ;
#17497=CARTESIAN_POINT ( 'NONE',  ( -2.449293598294706907E-16, 4.000000000000000000, -2.949999999999997957 ) ) ;
#17522=CARTESIAN_POINT ( 'NONE',  ( -1.432654583217641164, -3.458734125000000326, -0.8249999986344030978 ) ) ;
#17533=CARTESIAN_POINT ( 'NONE',  ( 2.445694354108820523, -2.445694354108820079, 0.1125000013655966247 ) ) ;
#17534=EDGE_LOOP ( 'NONE', ( #17909, #322, #5771, #22645 ) ) ;
#17546=CARTESIAN_POINT ( 'NONE',  ( 0.000000000000000000, 0.000000000000000000, 0.000000000000000000 ) ) ;
#17547=COLOUR_RGB ( '', 0.31764706, 0.68627451, 0.89019608) ;
#17555=CARTESIAN_POINT ( 'NONE',  ( -2.117863837641485618E-16, 3.458734125000000770, -0.2624999986344037084 ) ) ;
#17565=CARTESIAN_POINT ( 'NONE',  ( -4.000000000000000000, -1.656854249492383246, 0.4875000027311865436 ) ) ;
#17583=CARTESIAN_POINT ( 'NONE',  ( 3.458734125000000326, 4.235727675282971730E-16, 5.237500001365596347 ) ) ;
#17623=CARTESIAN_POINT ( 'NONE',  ( -4.000000000000000000, -1.656854249492383246, -2.637499999999998845 ) ) ;
#17625=CARTESIAN_POINT ( 'NONE',  ( -2.828427124746189403, -2.828427124746190735, 0.5500000027311869877 ) ) ;
#17631=ORIENTED_EDGE ( 'NONE', *, *, #10991, .T. ) ;
#17645=CARTESIAN_POINT ( 'NONE',  ( -2.445694354108820523, 2.445694354108820523, 0.8625000013655955700 ) ) ;
#17646=FACE_OUTER_BOUND ( 'NONE', #20809, .T. ) ;
#17649=DIRECTION ( 'NONE',  ( -1.000000000000000000, 0.000000000000000000, -0.000000000000000000 ) ) ;
#17671=CARTESIAN_POINT ( 'NONE',  ( -3.458734125000000770, 1.432654583217640498, 2.925000001365598123 ) ) ;
#17679=CARTESIAN_POINT ( 'NONE',  ( -2.828427124746189403, -2.828427124746190735, 1.550000002731187765 ) ) ;
#17693=FACE_OUTER_BOUND ( 'NONE', #20270, .T. ) ;
#17697=CARTESIAN_POINT ( 'NONE',  ( 6.353591512924457348E-16, -3.458734125000000326, 3.987500001365595015 ) ) ;
#17702=CARTESIAN_POINT ( 'NONE',  ( -2.977338099904818236, 2.250880586719687493, 2.039999999999999591 ) ) ;
#17703=CARTESIAN_POINT ( 'NONE',  ( -6.500000000000000000, 3.752776749732573247, -3.119443416399232394 ) ) ;
#17704=CARTESIAN_POINT ( 'NONE',  ( -4.000000000000000000, 0.000000000000000000, -1.699999999999998401 ) ) ;
#17718=CARTESIAN_POINT ( 'NONE',  ( 3.007318562400188799, 2.637429632093199139, 2.039999999999998259 ) ) ;
#17727=DIRECTION ( 'NONE',  ( -0.5000000000000007772, -0.8660254037844382635, 0.000000000000000000 ) ) ;
#17734=CARTESIAN_POINT ( 'NONE',  ( 5.432802636760778903, -4.368923434677197903, -0.2573354458087873109 ) ) ;
#17752=CARTESIAN_POINT ( 'NONE',  ( -1.432654583217641164, -3.458734125000000326, 0.1750000013655959585 ) ) ;
#17763=CARTESIAN_POINT ( 'NONE',  ( -2.445694354108819635, -2.445694354108820523, -3.137499998634404541 ) ) ;
#17780=CARTESIAN_POINT ( 'NONE',  ( 3.458734125000000770, 4.235727675282972223E-16, 2.487500001365596791 ) ) ;
#17781=CARTESIAN_POINT ( 'NONE',  ( 0.6867006470895935522, -3.397451134755354207, 2.039999999999998703 ) ) ;
#17785=DIRECTION ( 'NONE',  ( -1.000000000000000000, 0.000000000000000000, 0.000000000000000000 ) ) ;
#17791=CARTESIAN_POINT ( 'NONE',  ( 4.000000000000000000, 1.656854249492381248, -0.01249999726881388662 ) ) ;
#17795=CARTESIAN_POINT ( 'NONE',  ( 2.974182810908596597, -5.788408252967910173, 3.144609816681590009E-17 ) ) ;
#17808=CARTESIAN_POINT ( 'NONE',  ( 1.432654583217639832, 3.458734125000000326, 3.425000001365596791 ) ) ;
#17812=ORIENTED_EDGE ( 'NONE', *, *, #12706, .T. ) ;
#17817=ORIENTED_EDGE ( 'NONE', *, *, #1168, .T. ) ;
#17829=CARTESIAN_POINT ( 'NONE',  ( -4.000000000000000000, -1.656854249492383024, -0.6374999999999969580 ) ) ;
#17843=DIRECTION ( 'NONE',  ( 1.000000000000000000, 0.000000000000000000, 0.000000000000000000 ) ) ;
#17847=CARTESIAN_POINT ( 'NONE',  ( 2.445694354108820523, -2.445694354108820079, -0.8874999986344025427 ) ) ;
#17865=CARTESIAN_POINT ( 'NONE',  ( 1.432654583217642275, -3.458734124999999882, -1.699999998634404097 ) ) ;
#17870=ADVANCED_FACE ( 'NONE', ( #23068 ), #6679, .F. ) ;
#17878=CARTESIAN_POINT ( 'NONE',  ( 1.432654583217639832, 3.458734125000000326, -1.574999998634403875 ) ) ;
#17881=EDGE_LOOP ( 'NONE', ( #1868, #7971, #6493, #14365 ) ) ;
#17892=LINE ( 'NONE', #21578, #13683 ) ;
#17896=CARTESIAN_POINT ( 'NONE',  ( -1.432654583217640498, 3.458734125000000770, -0.1999999986344043745 ) ) ;
#17897=DIRECTION ( 'NONE',  ( 0.000000000000000000, 0.000000000000000000, -1.000000000000000000 ) ) ;
#17898=EDGE_CURVE ( 'NONE', #10786, #7079, #6992, .T. ) ;
#17906=CARTESIAN_POINT ( 'NONE',  ( -2.449293598294706907E-16, 4.000000000000000000, 1.175000002731187543 ) ) ;
#17909=ORIENTED_EDGE ( 'NONE', *, *, #16249, .T. ) ;
#17923=CARTESIAN_POINT ( 'NONE',  ( 3.458734125000000770, -1.432654583217639610, 5.175000001365595459 ) ) ;
#17926=CARTESIAN_POINT ( 'NONE',  ( 1.656854249492380138, 4.000000000000000000, -0.01249999999999832148 ) ) ;
#17952=CARTESIAN_POINT ( 'NONE',  ( -2.828427124746189403, -2.828427124746190735, -1.449999997268811347 ) ) ;
#17964=CARTESIAN_POINT ( 'NONE',  ( 2.445694354108820523, -2.445694354108820079, -1.887499998634403431 ) ) ;
#17971=DIRECTION ( 'NONE',  ( -1.000000000000000000, 0.000000000000000000, -0.000000000000000000 ) ) ;
#17987=CARTESIAN_POINT ( 'NONE',  ( -1.432654583217640498, 3.458734125000000770, -0.1999999986344043745 ) ) ;
#17998=CARTESIAN_POINT ( 'NONE',  ( 3.458734125000001214, -1.432654583217639610, -2.824999998634404541 ) ) ;
#18018=CARTESIAN_POINT ( 'NONE',  ( -2.445694354108819635, -2.445694354108820967, -1.887499998634403431 ) ) ;
#18027=CARTESIAN_POINT ( 'NONE',  ( 2.828427124746190735, -2.828427124746189847, 1.800000002731187987 ) ) ;
#18029=VERTEX_POINT ( 'NONE', #18159 ) ;
#18042=CARTESIAN_POINT ( 'NONE',  ( 6.500000000000000000, 3.752776749732563477, -3.700000000000000178 ) ) ;
#18045=CARTESIAN_POINT ( 'NONE',  ( -3.458734124999999882, -1.432654583217642497, 1.800000001365597235 ) ) ;
#18057=DIRECTION ( 'NONE',  ( 0.000000000000000000, 0.000000000000000000, 1.000000000000000000 ) ) ;
#18082=CARTESIAN_POINT ( 'NONE',  ( -2.445694354108820523, 2.445694354108820523, -3.387499998634403209 ) ) ;
#18098=DIRECTION ( 'NONE',  ( 1.000000000000000000, 0.000000000000000000, 0.000000000000000000 ) ) ;
#18100=CARTESIAN_POINT ( 'NONE',  ( 2.828427124746190735, -2.828427124746189847, 3.675000000000002931 ) ) ;
#18101=CARTESIAN_POINT ( 'NONE',  ( 7.347880794884118750E-16, -4.000000000000000000, 0.5500000000000018208 ) ) ;
#18128=EDGE_CURVE ( 'NONE', #8065, #10786, #15266, .T. ) ;
#18136=CARTESIAN_POINT ( 'NONE',  ( -1.656854249492381248, -3.999999999999999112, -3.387499997268812901 ) ) ;
#18143=CARTESIAN_POINT ( 'NONE',  ( -2.828427124746190291, 2.828427124746190291, -2.699999997268812457 ) ) ;
#18156=CARTESIAN_POINT ( 'NONE',  ( -3.458734125000000326, 0.000000000000000000, 1.737500001365596347 ) ) ;
#18159=CARTESIAN_POINT ( 'NONE',  ( 6.500000000000000888, 0.000000000000000000, -3.700000000000000178 ) ) ;
#18168=EDGE_LOOP ( 'NONE', ( #12705, #14126, #16379 ) ) ;
#18171=ORIENTED_EDGE ( 'NONE', *, *, #6502, .F. ) ;
#18198=CARTESIAN_POINT ( 'NONE',  ( 3.250000000000001776, -5.629165124598848990, 1.734723475976807094E-15 ) ) ;
#18206=CARTESIAN_POINT ( 'NONE',  ( 0.000000000000000000, 3.399999999999999911, 2.039999999999998259 ) ) ;
#18216=CARTESIAN_POINT ( 'NONE',  ( 2.445694354108820967, -2.445694354108820079, -2.637499998634404097 ) ) ;
#18248=CARTESIAN_POINT ( 'NONE',  ( -2.449293598294706907E-16, 4.000000000000000000, -3.824999997268811569 ) ) ;
#18260=CARTESIAN_POINT ( 'NONE',  ( 2.445694354108820079, 2.445694354108820523, 0.6125000013655953479 ) ) ;
#18263=ADVANCED_FACE ( 'NONE', ( #17348 ), #10587, .T. ) ;
#18267=CARTESIAN_POINT ( 'NONE',  ( 3.458734125000000326, 4.235727675282971730E-16, -1.762499998634403209 ) ) ;
#18269=CARTESIAN_POINT ( 'NONE',  ( -4.000000000000000000, 0.000000000000000000, 0.3000000000000016542 ) ) ;
#18279=VECTOR ( 'NONE', #23414, 1000.000000000000000 ) ;
#18281=( GEOMETRIC_REPRESENTATION_CONTEXT ( 3 ) GLOBAL_UNCERTAINTY_ASSIGNED_CONTEXT ( ( #666 ) ) GLOBAL_UNIT_ASSIGNED_CONTEXT ( ( #20509, #16941, #22553 ) ) REPRESENTATION_CONTEXT ( 'NONE', 'WORKASPACE' ) );
#18304=CARTESIAN_POINT ( 'NONE',  ( -2.117863837641482907E-16, 3.458734125000000770, -3.273533850472710061 ) ) ;
#18315=CYLINDRICAL_SURFACE ( 'NONE', #13225, 4.000000000000000000 ) ;
#18316=CARTESIAN_POINT ( 'NONE',  ( -3.458734125000000326, 0.000000000000000000, -3.262499998634404541 ) ) ;
#18320=ORIENTED_EDGE ( 'NONE', *, *, #23560, .F. ) ;
#18325=CARTESIAN_POINT ( 'NONE',  ( 0.000000000000000000, 0.000000000000000000, -3.700000000000000178 ) ) ;
#18340=CARTESIAN_POINT ( 'NONE',  ( -1.656854249492381248, -3.999999999999999112, 4.487499999999999822 ) ) ;
#18350=CONICAL_SURFACE ( 'NONE', #8041, 6.500000000000000888, 1.047197551196596521 ) ;
#18361=FACE_OUTER_BOUND ( 'NONE', #22877, .T. ) ;
#18370=CARTESIAN_POINT ( 'NONE',  ( -3.270501301980698550, -1.125461230421587633, 2.040000000000001812 ) ) ;
#18374=CARTESIAN_POINT ( 'NONE',  ( -2.828427124746190291, 2.828427124746190291, -2.699999997268812457 ) ) ;
#18383=CARTESIAN_POINT ( 'NONE',  ( 3.458734125000001214, -1.432654583217639610, 0.4250000013655961251 ) ) ;
#18389=CARTESIAN_POINT ( 'NONE',  ( 3.458734125000000326, 1.432654583217640498, 1.300000001365597235 ) ) ;
#18396=CARTESIAN_POINT ( 'NONE',  ( 6.500000000000000000, -3.142418015001832376, -3.295638806298775147 ) ) ;
#18401=EDGE_LOOP ( 'NONE', ( #2356, #490, #21213, #23159 ) ) ;
#18413=ORIENTED_EDGE ( 'NONE', *, *, #21650, .T. ) ;
#18449=CARTESIAN_POINT ( 'NONE',  ( 0.000000000000000000, 0.000000000000000000, 19.04999999999996874 ) ) ;
#18452=CARTESIAN_POINT ( 'NONE',  ( 1.432654583217642275, -3.458734124999999882, -2.699999998634404541 ) ) ;
#18467=VERTEX_POINT ( 'NONE', #19591 ) ;
#18484=CARTESIAN_POINT ( 'NONE',  ( 4.000000000000000888, -1.656854249492379694, -2.137499997268812013 ) ) ;
#18488=ORIENTED_EDGE ( 'NONE', *, *, #7967, .F. ) ;
#18491=CARTESIAN_POINT ( 'NONE',  ( -4.000000000000000000, 0.000000000000000000, -2.699999999999999289 ) ) ;
#18498=CARTESIAN_POINT ( 'NONE',  ( 2.503708927703406609E-30, 1.503597262882131219E-46, -0.8737698471611414774 ) ) ;
#18500=CARTESIAN_POINT ( 'NONE',  ( 3.458734125000000770, -1.432654583217639610, 0.1750000013655959585 ) ) ;
#18528=CARTESIAN_POINT ( 'NONE',  ( -2.117863837641485618E-16, 3.458734125000000770, -3.262499998634402765 ) ) ;
#18552=DIRECTION ( 'NONE',  ( 1.000000000000000000, 0.000000000000000000, 0.000000000000000000 ) ) ;
#18554=CARTESIAN_POINT ( 'NONE',  ( 0.000000000000000000, 0.000000000000000000, 0.000000000000000000 ) ) ;
#18558=CARTESIAN_POINT ( 'NONE',  ( 5.434916218090830142, 4.367703157927330437, -0.2578475836320699988 ) ) ;
#18565=CARTESIAN_POINT ( 'NONE',  ( 3.458734125000000770, 4.235727675282972223E-16, -0.5124999986344038749 ) ) ;
#18566=CARTESIAN_POINT ( 'NONE',  ( 4.000000000000000888, -1.656854249492379694, 5.737500000000000711 ) ) ;
#18567=CARTESIAN_POINT ( 'NONE',  ( 2.828427124746190735, -2.828427124746189847, -3.199999997268812901 ) ) ;
#18605=CARTESIAN_POINT ( 'NONE',  ( -2.445694354108819635, -2.445694354108820523, 3.862500001365594571 ) ) ;
#18606=CARTESIAN_POINT ( 'NONE',  ( 1.763857611550045723, 3.892996637942334637, 1.981791682344426375 ) ) ;
#18622=CARTESIAN_POINT ( 'NONE',  ( -1.432654583217640498, 3.458734125000000770, 4.800000001365595459 ) ) ;
#18631=CARTESIAN_POINT ( 'NONE',  ( 0.000000000000000000, 0.000000000000000000, 0.000000000000000000 ) ) ;
#18652=CARTESIAN_POINT ( 'NONE',  ( 3.422634207080918589, -1.398009529842456855, 2.039999999999996927 ) ) ;
#18670=CARTESIAN_POINT ( 'NONE',  ( 0.2615509004163102946, 3.991439731035835603, 2.039999999999998259 ) ) ;
#18671=ORIENTED_EDGE ( 'NONE', *, *, #18128, .F. ) ;
#18673=CARTESIAN_POINT ( 'NONE',  ( -4.000000000000000000, -1.656854249492383024, 1.362500000000001377 ) ) ;
#18689=CARTESIAN_POINT ( 'NONE',  ( -1.432654583217641164, -3.458734125000000326, -1.824999998634404097 ) ) ;
#18690=CARTESIAN_POINT ( 'NONE',  ( -1.656854249492381248, -3.999999999999999112, 2.487500000000002043 ) ) ;
#18718=CARTESIAN_POINT ( 'NONE',  ( -3.458734125000000770, 1.432654583217640498, 3.925000001365594127 ) ) ;
#18728=SHAPE_REPRESENTATION_RELATIONSHIP ( 'NONE' , 'NONE' ,  #1939, #8790 ) ;
#18729=CARTESIAN_POINT ( 'NONE',  ( -3.458734124999999882, -1.432654583217642497, 1.800000001365597235 ) ) ;
#18731=CARTESIAN_POINT ( 'NONE',  ( -3.802871176606132053, -5.309964801958122926, -0.01372220897662011427 ) ) ;
#18739=ADVANCED_FACE ( 'NONE', ( #2810, #7988 ), #1010, .T. ) ;
#18742=CARTESIAN_POINT ( 'NONE',  ( -2.445694354108819635, -2.445694354108820967, -0.8874999986344025427 ) ) ;
#18744=AXIS2_PLACEMENT_3D ( 'NONE', #18449, #7568, #18098 ) ;
#18751=CARTESIAN_POINT ( 'NONE',  ( -2.445694354108819635, -2.445694354108820967, 5.112500001365595459 ) ) ;
#18762=EDGE_LOOP ( 'NONE', ( #19896, #2246, #13889, #16232 ) ) ;
#18763=CARTESIAN_POINT ( 'NONE',  ( 0.000000000000000000, 0.000000000000000000, -3.700000000000000178 ) ) ;
#18780=CARTESIAN_POINT ( 'NONE',  ( -2.696295709017760611, -5.948846446048907666, -3.700000000000000622 ) ) ;
#18798=CARTESIAN_POINT ( 'NONE',  ( 7.347880794884118750E-16, -4.000000000000000000, 1.550000000000000933 ) ) ;
#18801=DIRECTION ( 'NONE',  ( -1.000000000000000000, 0.000000000000000000, 0.000000000000000000 ) ) ;
#18810=CARTESIAN_POINT ( 'NONE',  ( 3.458734125000000770, 4.235727675282972223E-16, -2.512499998634404097 ) ) ;
#18811=CARTESIAN_POINT ( 'NONE',  ( 4.000000000000000000, 4.898587196589412829E-16, -0.1999999999999987899 ) ) ;
#18834=CARTESIAN_POINT ( 'NONE',  ( 1.432654583217642275, -3.458734124999999882, 2.300000001365597679 ) ) ;
#18837=EDGE_CURVE ( 'NONE', #20113, #23104, #16162, .T. ) ;
#18843=CARTESIAN_POINT ( 'NONE',  ( 3.458734125000000770, -1.432654583217639610, 3.175000001365598568 ) ) ;
#18844=CARTESIAN_POINT ( 'NONE',  ( -3.458734124999999882, -1.432654583217642275, 0.8000000013655964581 ) ) ;
#18845=VERTEX_POINT ( 'NONE', #11598 ) ;
#18860=CONICAL_SURFACE ( 'NONE', #22285, 6.500000000000000888, 1.047197551196596521 ) ;
#18861=CARTESIAN_POINT ( 'NONE',  ( -3.458734125000000770, 0.000000000000000000, 5.987500001365596347 ) ) ;
#18868=CARTESIAN_POINT ( 'NONE',  ( -2.828427124746190291, 2.828427124746190291, 4.300000002731186655 ) ) ;
#18904=CARTESIAN_POINT ( 'NONE',  ( 3.802871176606126280, 5.309964801958114045, -3.686277791023383266 ) ) ;
#18909=CARTESIAN_POINT ( 'NONE',  ( 0.000000000000000000, 0.000000000000000000, 19.04999999999996874 ) ) ;
#18924=CARTESIAN_POINT ( 'NONE',  ( 2.828427124746190735, -2.828427124746189847, 0.6750000000000020428 ) ) ;
#18935=ORIENTED_EDGE ( 'NONE', *, *, #15650, .F. ) ;
#18948=CARTESIAN_POINT ( 'NONE',  ( -1.432654583217640498, 3.458734125000000770, 4.800000001365595459 ) ) ;
#18957=CARTESIAN_POINT ( 'NONE',  ( 2.445694354108820523, -2.445694354108820079, 2.112500001365596791 ) ) ;
#18960=FACE_OUTER_BOUND ( 'NONE', #9322, .T. ) ;
#18968=CARTESIAN_POINT ( 'NONE',  ( 3.458734125000001214, -1.432654583217639610, -1.574999998634403875 ) ) ;
#18975=CARTESIAN_POINT ( 'NONE',  ( 2.445694354108820079, 2.445694354108820523, 3.612500001365598123 ) ) ;
#18982=CARTESIAN_POINT ( 'NONE',  ( -4.000000000000000888, 1.656854249492380804, 3.362500002731190651 ) ) ;
#18991=DIRECTION ( 'NONE',  ( 1.000000000000000000, 0.000000000000000000, 0.000000000000000000 ) ) ;
#18997=DIRECTION ( 'NONE',  ( -0.000000000000000000, -0.000000000000000000, 1.000000000000000000 ) ) ;
#19005=( BOUNDED_SURFACE ( )  B_SPLINE_SURFACE ( 1, 2, ( 
 ( #12204, #23309, #2828, #12437, #8597, #12087, #1149, #17466, #17583, #17923, #4997, #23428, #16020, #10417, #19476, #23180, #19352, #16142, #2941, #15903, #3305, #8365, #1508, #3073, #13990, #12325, #21252, #1030, #17697, #3184, #21492, #7034, #21612, #8490, #19588, #13880, #10530, #17808, #15683, #22956, #6918, #14352, #10294, #5219, #12564, #10648, #6564, #1258, #14236, #4869, #1376, #21138, #4751, #15794, #6791, #23066, #14112, #8714, #21375, #5105, #5576, #13029, #7629, #18045, #18156, #23545, #1622, #10771, #3771, #21733, #16487, #18389, #20049, #9077, #16599, #5694, #5460, #12796, #14823, #7153, #14707, #5814, #20289, #19824, #14951, #11111, #16715, #293, #16255, #18500, #2086, #22203, #3430, #16368, #22076, #23664, #14467, #7395, #3890, #3653, #12904, #20164, #8965, #5345, #7510, #12689, #1969, #19943, #9309, #3543, #179, #21964, #11226, #9426, #10878, #1738, #7281, #14594, #21854, #10988, #18267, #1852, #9201, #63, #15181, #9781, #422, #11708, #8112, #22803, #17076, #15065, #15539, #4013, #13385, #13614, #20876, #11350, #11475, #6181, #15421, #779, #4133, #13141, #19100, #20405, #11593, #2558, #6297 ),
 ( #18861, #22685, #2692, #4485, #650, #9906, #7983, #17320, #22320, #17201, #11825, #10032, #2446, #886, #18751, #2335, #8221, #7749, #20654, #18622, #2209, #13501, #9548, #16845, #5936, #20525, #9668, #13262, #16958, #535, #4258, #6053, #15303, #22440, #7858, #22577, #20766, #4369, #18975, #16114, #12174, #13856, #20996, #4616, #8466, #1005, #8816, #21228, #2805, #17671, #12299, #8337, #10265, #4728, #15770, #8687, #17780, #1232, #19444, #12060, #1121, #10501, #6765, #6654, #1473, #15878, #8571, #14207, #19561, #21344, #6886, #15992, #5077, #19215, #21464, #10146, #19327, #3155, #23276, #23042, #3041, #17440, #4968, #1353, #6417, #10390, #15655, #13732, #11950, #13966, #12409, #19674, #22927, #2915, #23154, #3280, #10622, #21111, #6540, #17896, #17555, #4840, #14081, #16907, #18565, #19918, #9617, #2278, #5194, #5766, #485, #5996, #7808, #20349, #20470, #2148, #4198, #8933, #13204, #22386, #4076, #13094, #13323, #21706, #12657, #18689, #18018, #7570, #20592, #14321, #363, #11541, #9726, #1594, #7126, #5315, #18810, #2393, #3396, #236, #16661, #3956, #2030, #21580, #11290, #22147, #23398, #9483, #7002 ) ),
 .UNSPECIFIED., .F., .F., .F. ) 
 B_SPLINE_SURFACE_WITH_KNOTS ( ( 2, 2 ),
 ( 3, 2, 2, 2, 2, 2, 2, 2, 2, 2, 2, 2, 2, 2, 2, 2, 2, 2, 2, 2, 2, 2, 2, 2, 2, 2, 2, 2, 2, 2, 2, 2, 2, 2, 2, 2, 2, 2, 2, 2, 2, 2, 2, 2, 2, 2, 2, 2, 2, 2, 2, 2, 2, 2, 2, 2, 2, 2, 2, 2, 2, 2, 2, 2, 2, 2, 2, 2, 2, 2, 2, 2, 2, 2, 3 ),
 ( 0.000000000000000000, 1.000000000000000000 ),
 ( 0.000000000000000000, 0.01250000000000000069, 0.02500000000000000139, 0.03749999999999999861, 0.05000000000000000278, 0.06250000000000000000, 0.07499999999999999722, 0.08749999999999999445, 0.1000000000000000056, 0.1125000000000000028, 0.1250000000000000000, 0.1375000000000000111, 0.1499999999999999944, 0.1625000000000000056, 0.1749999999999999889, 0.1875000000000000000, 0.2000000000000000111, 0.2124999999999999944, 0.2250000000000000056, 0.2374999999999999889, 0.2500000000000000000, 0.2625000000000000111, 0.2750000000000000222, 0.2874999999999999778, 0.2999999999999999889, 0.3125000000000000000, 0.3250000000000000111, 0.3375000000000000222, 0.3499999999999999778, 0.3624999999999999889, 0.3750000000000000000, 0.3875000000000000111, 0.4000000000000000222, 0.4124999999999999778, 0.4249999999999999889, 0.4375000000000000000, 0.4500000000000000111, 0.4625000000000000222, 0.4749999999999999778, 0.4874999999999999889, 0.5000000000000000000, 0.5124999999999999556, 0.5250000000000000222, 0.5374999999999999778, 0.5500000000000000444, 0.5625000000000000000, 0.5749999999999999556, 0.5875000000000000222, 0.5999999999999999778, 0.6125000000000000444, 0.6250000000000000000, 0.6374999999999999556, 0.6500000000000000222, 0.6624999999999999778, 0.6750000000000000444, 0.6875000000000000000, 0.6999999999999999556, 0.7125000000000000222, 0.7249999999999999778, 0.7375000000000000444, 0.7500000000000000000, 0.7624999999999999556, 0.7750000000000000222, 0.7874999999999999778, 0.8000000000000000444, 0.8125000000000000000, 0.8249999999999999556, 0.8375000000000000222, 0.8499999999999999778, 0.8625000000000000444, 0.8750000000000000000, 0.8874999999999999556, 0.9000000000000000222, 0.9124999999999999778, 0.9250000000000000444 ),
 .UNSPECIFIED. ) 
 GEOMETRIC_REPRESENTATION_ITEM ( )  RATIONAL_B_SPLINE_SURFACE ( (
 ( 1.000000000000000000, 0.9238795325112867385, 1.000000000000000000, 0.9238795325112867385, 1.000000000000000000, 0.9238795325112867385, 1.000000000000000000, 0.9238795325112867385, 1.000000000000000000, 0.9238795325112867385, 1.000000000000000000, 0.9238795325112867385, 1.000000000000000000, 0.9238795325112867385, 1.000000000000000000, 0.9238795325112867385, 1.000000000000000000, 0.9238795325112867385, 1.000000000000000000, 0.9238795325112867385, 1.000000000000000000, 0.9238795325112867385, 1.000000000000000000, 0.9238795325112867385, 1.000000000000000000, 0.9238795325112867385, 1.000000000000000000, 0.9238795325112867385, 1.000000000000000000, 0.9238795325112867385, 1.000000000000000000, 0.9238795325112867385, 1.000000000000000000, 0.9238795325112867385, 1.000000000000000000, 0.9238795325112867385, 1.000000000000000000, 0.9238795325112867385, 1.000000000000000000, 0.9238795325112867385, 1.000000000000000000, 0.9238795325112867385, 1.000000000000000000, 0.9238795325112867385, 1.000000000000000000, 0.9238795325112867385, 1.000000000000000000, 0.9238795325112867385, 1.000000000000000000, 0.9238795325112867385, 1.000000000000000000, 0.9238795325112867385, 1.000000000000000000, 0.9238795325112867385, 1.000000000000000000, 0.9238795325112867385, 1.000000000000000000, 0.9238795325112867385, 1.000000000000000000, 0.9238795325112867385, 1.000000000000000000, 0.9238795325112867385, 1.000000000000000000, 0.9238795325112867385, 1.000000000000000000, 0.9238795325112867385, 1.000000000000000000, 0.9238795325112867385, 1.000000000000000000, 0.9238795325112867385, 1.000000000000000000, 0.9238795325112867385, 1.000000000000000000, 0.9238795325112867385, 1.000000000000000000, 0.9238795325112867385, 1.000000000000000000, 0.9238795325112867385, 1.000000000000000000, 0.9238795325112867385, 1.000000000000000000, 0.9238795325112867385, 1.000000000000000000, 0.9238795325112867385, 1.000000000000000000, 0.9238795325112867385, 1.000000000000000000, 0.9238795325112867385, 1.000000000000000000, 0.9238795325112867385, 1.000000000000000000, 0.9238795325112867385, 1.000000000000000000, 0.9238795325112867385, 1.000000000000000000, 0.9238795325112867385, 1.000000000000000000, 0.9238795325112867385, 1.000000000000000000, 0.9238795325112867385, 1.000000000000000000, 0.9238795325112867385, 1.000000000000000000, 0.9238795325112867385, 1.000000000000000000, 0.9238795325112867385, 1.000000000000000000, 0.9238795325112867385, 1.000000000000000000, 0.9238795325112867385, 1.000000000000000000, 0.9238795325112867385, 1.000000000000000000, 0.9238795325112867385, 1.000000000000000000, 0.9238795325112867385, 1.000000000000000000, 0.9238795325112867385, 1.000000000000000000, 0.9238795325112867385, 1.000000000000000000, 0.9238795325112867385, 1.000000000000000000, 0.9238795325112867385, 1.000000000000000000, 0.9238795325112867385, 1.000000000000000000, 0.9238795325112867385, 1.000000000000000000, 0.9238795325112867385, 1.000000000000000000, 0.9238795325112867385, 1.000000000000000000, 0.9238795325112867385, 1.000000000000000000, 0.9238795325112867385, 1.000000000000000000, 0.9238795325112867385, 1.000000000000000000, 0.9238795325112867385, 1.000000000000000000, 0.9238795325112867385, 1.000000000000000000, 0.9238795325112867385, 1.000000000000000000, 0.9238795325112867385, 1.000000000000000000, 0.9238795325112867385, 1.000000000000000000),
 ( 1.000000000000000000, 0.9238795325112867385, 1.000000000000000000, 0.9238795325112867385, 1.000000000000000000, 0.9238795325112867385, 1.000000000000000000, 0.9238795325112867385, 1.000000000000000000, 0.9238795325112867385, 1.000000000000000000, 0.9238795325112867385, 1.000000000000000000, 0.9238795325112867385, 1.000000000000000000, 0.9238795325112867385, 1.000000000000000000, 0.9238795325112867385, 1.000000000000000000, 0.9238795325112867385, 1.000000000000000000, 0.9238795325112867385, 1.000000000000000000, 0.9238795325112867385, 1.000000000000000000, 0.9238795325112867385, 1.000000000000000000, 0.9238795325112867385, 1.000000000000000000, 0.9238795325112867385, 1.000000000000000000, 0.9238795325112867385, 1.000000000000000000, 0.9238795325112867385, 1.000000000000000000, 0.9238795325112867385, 1.000000000000000000, 0.9238795325112867385, 1.000000000000000000, 0.9238795325112867385, 1.000000000000000000, 0.9238795325112867385, 1.000000000000000000, 0.9238795325112867385, 1.000000000000000000, 0.9238795325112867385, 1.000000000000000000, 0.9238795325112867385, 1.000000000000000000, 0.9238795325112867385, 1.000000000000000000, 0.9238795325112867385, 1.000000000000000000, 0.9238795325112867385, 1.000000000000000000, 0.9238795325112867385, 1.000000000000000000, 0.9238795325112867385, 1.000000000000000000, 0.9238795325112867385, 1.000000000000000000, 0.9238795325112867385, 1.000000000000000000, 0.9238795325112867385, 1.000000000000000000, 0.9238795325112867385, 1.000000000000000000, 0.9238795325112867385, 1.000000000000000000, 0.9238795325112867385, 1.000000000000000000, 0.9238795325112867385, 1.000000000000000000, 0.9238795325112867385, 1.000000000000000000, 0.9238795325112867385, 1.000000000000000000, 0.9238795325112867385, 1.000000000000000000, 0.9238795325112867385, 1.000000000000000000, 0.9238795325112867385, 1.000000000000000000, 0.9238795325112867385, 1.000000000000000000, 0.9238795325112867385, 1.000000000000000000, 0.9238795325112867385, 1.000000000000000000, 0.9238795325112867385, 1.000000000000000000, 0.9238795325112867385, 1.000000000000000000, 0.9238795325112867385, 1.000000000000000000, 0.9238795325112867385, 1.000000000000000000, 0.9238795325112867385, 1.000000000000000000, 0.9238795325112867385, 1.000000000000000000, 0.9238795325112867385, 1.000000000000000000, 0.9238795325112867385, 1.000000000000000000, 0.9238795325112867385, 1.000000000000000000, 0.9238795325112867385, 1.000000000000000000, 0.9238795325112867385, 1.000000000000000000, 0.9238795325112867385, 1.000000000000000000, 0.9238795325112867385, 1.000000000000000000, 0.9238795325112867385, 1.000000000000000000, 0.9238795325112867385, 1.000000000000000000, 0.9238795325112867385, 1.000000000000000000, 0.9238795325112867385, 1.000000000000000000, 0.9238795325112867385, 1.000000000000000000, 0.9238795325112867385, 1.000000000000000000, 0.9238795325112867385, 1.000000000000000000, 0.9238795325112867385, 1.000000000000000000, 0.9238795325112867385, 1.000000000000000000, 0.9238795325112867385, 1.000000000000000000, 0.9238795325112867385, 1.000000000000000000, 0.9238795325112867385, 1.000000000000000000, 0.9238795325112867385, 1.000000000000000000, 0.9238795325112867385, 1.000000000000000000, 0.9238795325112867385, 1.000000000000000000, 0.9238795325112867385, 1.000000000000000000, 0.9238795325112867385, 1.000000000000000000) ) ) 
 REPRESENTATION_ITEM ( '' )  SURFACE ( )  );
#19016=VERTEX_POINT ( 'NONE', #12414 ) ;
#19039=CARTESIAN_POINT ( 'NONE',  ( 4.000000000000000000, 1.656854249492381248, 2.862500000000002043 ) ) ;
#19058=CARTESIAN_POINT ( 'NONE',  ( -2.449293598294706907E-16, 4.000000000000000000, -3.674599999999999866 ) ) ;
#19069=CARTESIAN_POINT ( 'NONE',  ( -3.458734125000000770, 1.432654583217640498, 1.925000001365597457 ) ) ;
#19078=CARTESIAN_POINT ( 'NONE',  ( 2.445694354108820079, 2.445694354108820523, 1.362500001365595903 ) ) ;
#19080=CARTESIAN_POINT ( 'NONE',  ( -2.445694354108819635, -2.445694354108820523, -1.137499998634402765 ) ) ;
#19094=AXIS2_PLACEMENT_3D ( 'NONE', #10316, #17252, #17365 ) ;
#19100=CARTESIAN_POINT ( 'NONE',  ( -3.458734125000000326, 0.000000000000000000, -3.262499998634404541 ) ) ;
#19111=CARTESIAN_POINT ( 'NONE',  ( -4.000000000000000000, -1.656854249492383246, 3.487500002731189319 ) ) ;
#19119=VECTOR ( 'NONE', #8845, 1000.000000000000000 ) ;
#19140=CIRCLE ( 'NONE', #15738, 6.500000000000000888 ) ;
#19143=CARTESIAN_POINT ( 'NONE',  ( 4.000000000000000000, 1.656854249492381248, 0.8625000000000004885 ) ) ;
#19159=DIRECTION ( 'NONE',  ( -1.000000000000000000, 0.000000000000000000, 0.000000000000000000 ) ) ;
#19161=CARTESIAN_POINT ( 'NONE',  ( -1.656854249492381248, -3.999999999999999112, 1.487500000000001377 ) ) ;
#19164=CARTESIAN_POINT ( 'NONE',  ( -2.449293598294706907E-16, 4.000000000000000000, -0.9499999999999977351 ) ) ;
#19165=ADVANCED_FACE ( 'NONE', ( #20140 ), #271, .F. ) ;
#19169=ORIENTED_EDGE ( 'NONE', *, *, #6631, .T. ) ;
#19187=CARTESIAN_POINT ( 'NONE',  ( -3.458734125000000770, 1.432654583217640498, 4.925000001365594571 ) ) ;
#19197=CARTESIAN_POINT ( 'NONE',  ( 6.353591512924457348E-16, -3.458734125000000326, -0.01249999863440348635 ) ) ;
#19198=CARTESIAN_POINT ( 'NONE',  ( -3.458734125000000326, 1.432654583217640276, 1.675000001365597235 ) ) ;
#19200=CARTESIAN_POINT ( 'NONE',  ( -5.479999999999998650, 6.711064459327494520E-16, 2.039999999999998259 ) ) ;
#19215=CARTESIAN_POINT ( 'NONE',  ( 3.458734125000001214, -1.432654583217639610, 1.425000001365596791 ) ) ;
#19234=AXIS2_PLACEMENT_3D ( 'NONE', #15993, #14322, #12769 ) ;
#19270=CARTESIAN_POINT ( 'NONE',  ( 4.000000000000000000, 4.898587196589412829E-16, -1.199999999999997957 ) ) ;
#19272=CARTESIAN_POINT ( 'NONE',  ( 4.000000000000000000, 0.000000000000000000, 19.04999999999996874 ) ) ;
#19279=CARTESIAN_POINT ( 'NONE',  ( -4.000000000000000888, 1.656854249492380582, -1.637499997268811569 ) ) ;
#19285=CARTESIAN_POINT ( 'NONE',  ( 6.500000000000000000, 3.752776749732573247, -3.119443416399232394 ) ) ;
#19294=CARTESIAN_POINT ( 'NONE',  ( -3.458734125000000326, -1.432654583217642497, 0.05000000136559582670 ) ) ;
#19304=CARTESIAN_POINT ( 'NONE',  ( -2.117863837641485618E-16, 3.458734125000000326, 0.4875000013655952369 ) ) ;
#19306=CARTESIAN_POINT ( 'NONE',  ( 0.000000000000000000, 0.000000000000000000, 0.000000000000000000 ) ) ;
#19327=CARTESIAN_POINT ( 'NONE',  ( 6.353591512924457348E-16, -3.458734125000000770, 1.237500001365595903 ) ) ;
#19336=CARTESIAN_POINT ( 'NONE',  ( -4.000000000000000888, 1.656854249492380804, -0.6374999972688125682 ) ) ;
#19344=ADVANCED_FACE ( 'NONE', ( #628 ), #6157, .F. ) ;
#19352=CARTESIAN_POINT ( 'NONE',  ( -3.458734125000000326, 0.000000000000000000, 4.737500001365595459 ) ) ;
#19358=CARTESIAN_POINT ( 'NONE',  ( -4.000000000000000000, 1.285413958923598443, -3.623488494345327382 ) ) ;
#19378=CARTESIAN_POINT ( 'NONE',  ( 0.000000000000000000, 0.000000000000000000, -3.700000000000000178 ) ) ;
#19382=CARTESIAN_POINT ( 'NONE',  ( 4.000000000000000000, 4.898587196589412829E-16, -2.199999999999998845 ) ) ;
#19384=DIRECTION ( 'NONE',  ( 0.000000000000000000, 0.000000000000000000, 1.000000000000000000 ) ) ;
#19408=CARTESIAN_POINT ( 'NONE',  ( 2.445694354108820967, -2.445694354108820079, 1.362500001365595903 ) ) ;
#19416=ORIENTED_EDGE ( 'NONE', *, *, #147, .F. ) ;
#19423=DIRECTION ( 'NONE',  ( -1.000000000000000000, 0.000000000000000000, 0.000000000000000000 ) ) ;
#19427=VERTEX_POINT ( 'NONE', #1326 ) ;
#19432=B_SPLINE_CURVE_WITH_KNOTS ( 'NONE', 3,
 ( #5842, #7424, #14734, #12716, #21993, #5607, #19968, #451 ),
 .UNSPECIFIED., .F., .F.,
 ( 4, 2, 2, 4 ),
 ( 0.003797433802554436334, 0.004743183970586237024, 0.005688934138618036845, 0.007580434474681636489 ),
 .UNSPECIFIED. ) ;
#19444=CARTESIAN_POINT ( 'NONE',  ( 2.445694354108820967, -2.445694354108820079, 2.362500001365596791 ) ) ;
#19456=CARTESIAN_POINT ( 'NONE',  ( 4.000000000000000000, 1.656854249492381248, -1.012499997268812901 ) ) ;
#19467=AXIS2_PLACEMENT_3D ( 'NONE', #359, #232, #2026 ) ;
#19468=CARTESIAN_POINT ( 'NONE',  ( -4.000000000000000000, 0.000000000000000000, 1.425000002731187765 ) ) ;
#19476=CARTESIAN_POINT ( 'NONE',  ( -2.445694354108819635, -2.445694354108820523, 4.862500001365595459 ) ) ;
#19481=CARTESIAN_POINT ( 'NONE',  ( -3.553888437116970778, 0.5218273788507123978, 2.039999999999990266 ) ) ;
#19483=CARTESIAN_POINT ( 'NONE',  ( -1.656854249492381248, -3.999999999999999112, -1.512499999999997735 ) ) ;
#19490=ORIENTED_EDGE ( 'NONE', *, *, #11134, .F. ) ;
#19502=DIRECTION ( 'NONE',  ( -0.000000000000000000, -0.000000000000000000, 1.000000000000000000 ) ) ;
#19511=CARTESIAN_POINT ( 'NONE',  ( -1.656854249492380804, 4.000000000000000000, -0.8874999999999971800 ) ) ;
#19516=CARTESIAN_POINT ( 'NONE',  ( 5.968343123267133343, -4.059728990630809164, -0.4033376246892532713 ) ) ;
#19533=CARTESIAN_POINT ( 'NONE',  ( -2.117863837641485618E-16, 3.458734125000000770, -1.262499998634402765 ) ) ;
#19547=DIRECTION ( 'NONE',  ( -0.000000000000000000, -0.000000000000000000, 1.000000000000000000 ) ) ;
#19554=DIRECTION ( 'NONE',  ( -0.000000000000000000, -0.000000000000000000, 1.000000000000000000 ) ) ;
#19561=CARTESIAN_POINT ( 'NONE',  ( -2.117863837641485618E-16, 3.458734125000000770, 1.737500001365596347 ) ) ;
#19569=CARTESIAN_POINT ( 'NONE',  ( 1.656854249492383024, -3.999999999999999112, -1.262499997268811347 ) ) ;
#19588=CARTESIAN_POINT ( 'NONE',  ( -2.445694354108820523, 2.445694354108820523, 3.612500001365594571 ) ) ;
#19591=CARTESIAN_POINT ( 'NONE',  ( 5.479999999999998650, 0.000000000000000000, 3.059999999999998277 ) ) ;
#19601=ORIENTED_EDGE ( 'NONE', *, *, #11760, .F. ) ;
#19605=ADVANCED_FACE ( 'NONE', ( #1413 ), #14026, .F. ) ;
#19607=CARTESIAN_POINT ( 'NONE',  ( 6.500000000000000000, 3.752776749732573247, -3.119443416399232394 ) ) ;
#19617=DIRECTION ( 'NONE',  ( 1.000000000000000000, 0.000000000000000000, 0.000000000000000000 ) ) ;
#19620=CARTESIAN_POINT ( 'NONE',  ( -2.828427124746189403, -2.828427124746190735, -1.574999999999998179 ) ) ;
#19627=CARTESIAN_POINT ( 'NONE',  ( 2.445694354108820079, 2.445694354108820523, -2.637499998634404097 ) ) ;
#19632=ORIENTED_EDGE ( 'NONE', *, *, #19706, .F. ) ;
#19646=CARTESIAN_POINT ( 'NONE',  ( -3.458734125000000770, 0.000000000000000000, -0.01249999863440348635 ) ) ;
#19650=CARTESIAN_POINT ( 'NONE',  ( -6.500000000000000000, 3.752776749732564809, -3.700000000000000178 ) ) ;
#19657=CARTESIAN_POINT ( 'NONE',  ( 3.458734125000000326, 4.235727675282971730E-16, -1.762499998634403209 ) ) ;
#19663=VERTEX_POINT ( 'NONE', #1071 ) ;
#19672=FACE_OUTER_BOUND ( 'NONE', #17534, .T. ) ;
#19674=CARTESIAN_POINT ( 'NONE',  ( 1.432654583217642275, -3.458734124999999882, 0.3000000013655960696 ) ) ;
#19675=CARTESIAN_POINT ( 'NONE',  ( 0.9097406175788815830, -3.344736155888329510, 2.040000000000001812 ) ) ;
#19684=CARTESIAN_POINT ( 'NONE',  ( 1.656854249492380360, 4.000000000000000000, 0.1125000027311862244 ) ) ;
#19706=EDGE_CURVE ( 'NONE', #19663, #15405, #4026, .T. ) ;
#19720=CARTESIAN_POINT ( 'NONE',  ( -4.000000000000000000, 0.000000000000000000, -0.6999999999999975131 ) ) ;
#19733=CARTESIAN_POINT ( 'NONE',  ( 2.828427124746190735, -2.828427124746189847, -1.199999997268811125 ) ) ;
#19740=CARTESIAN_POINT ( 'NONE',  ( -0.3925654445992010633, 3.441971588417507721, -3.295601554149321988 ) ) ;
#19746=CARTESIAN_POINT ( 'NONE',  ( 6.353591512924457348E-16, -3.458734125000000326, -1.012499998634402543 ) ) ;
#19749=ORIENTED_EDGE ( 'NONE', *, *, #13319, .T. ) ;
#19764=CARTESIAN_POINT ( 'NONE',  ( 2.445694354108820967, -2.445694354108820079, -0.6374999986344023206 ) ) ;
#19776=ADVANCED_FACE ( 'NONE', ( #5742 ), #18315, .F. ) ;
#19806=CARTESIAN_POINT ( 'NONE',  ( 4.000000000000000000, 4.898587196589412829E-16, 1.925000002731188209 ) ) ;
#19816=( GEOMETRIC_REPRESENTATION_CONTEXT ( 3 ) GLOBAL_UNCERTAINTY_ASSIGNED_CONTEXT ( ( #11965 ) ) GLOBAL_UNIT_ASSIGNED_CONTEXT ( ( #10127, #10017, #8096 ) ) REPRESENTATION_CONTEXT ( 'NONE', 'WORKASPACE' ) );
#19817=DIRECTION ( 'NONE',  ( 0.000000000000000000, 0.000000000000000000, -1.000000000000000000 ) ) ;
#19821=DIRECTION ( 'NONE',  ( 1.000000000000000000, 0.000000000000000000, 0.000000000000000000 ) ) ;
#19824=CARTESIAN_POINT ( 'NONE',  ( -1.432654583217640276, 3.458734125000000326, 0.5500000013655963471 ) ) ;
#19833=VERTEX_POINT ( 'NONE', #9240 ) ;
#19839=CARTESIAN_POINT ( 'NONE',  ( -6.499999999999999112, -1.264206540070615281, -0.05450957050772532037 ) ) ;
#19852=DIRECTION ( 'NONE',  ( -1.000000000000000000, 0.000000000000000000, 0.000000000000000000 ) ) ;
#19864=DIRECTION ( 'NONE',  ( -0.000000000000000000, -0.000000000000000000, 1.000000000000000000 ) ) ;
#19866=DIRECTION ( 'NONE',  ( -0.000000000000000000, -0.000000000000000000, 1.000000000000000000 ) ) ;
#19867=CARTESIAN_POINT ( 'NONE',  ( -3.458734124999999882, -1.432654583217642497, -1.199999998634403431 ) ) ;
#19873=FACE_BOUND ( 'NONE', #21504, .T. ) ;
#19876=CARTESIAN_POINT ( 'NONE',  ( 4.000000000000000000, 4.898587196589412829E-16, -1.074999997268812679 ) ) ;
#19889=CARTESIAN_POINT ( 'NONE',  ( 4.000000000000000888, -1.656854249492379694, 3.737500000000002931 ) ) ;
#19896=ORIENTED_EDGE ( 'NONE', *, *, #3099, .T. ) ;
#19900=CARTESIAN_POINT ( 'NONE',  ( 3.458734125000000326, 4.235727675282971730E-16, -2.762499998634404097 ) ) ;
#19918=CARTESIAN_POINT ( 'NONE',  ( 3.458734125000001214, -1.432654583217639610, -0.5749999986344027647 ) ) ;
#19919=CARTESIAN_POINT ( 'NONE',  ( -0.4410157350360267015, -3.437995502366750777, 2.040000000000000480 ) ) ;
#19926=CARTESIAN_POINT ( 'NONE',  ( -2.449293598294706907E-16, 4.000000000000000000, -2.824999997268812457 ) ) ;
#19936=DIRECTION ( 'NONE',  ( 1.000000000000000000, 0.000000000000000000, 0.000000000000000000 ) ) ;
#19943=CARTESIAN_POINT ( 'NONE',  ( 1.432654583217642275, -3.458734124999999437, -0.9499999986344030978 ) ) ;
#19968=CARTESIAN_POINT ( 'NONE',  ( 0.5303295852573085556, -7.199367570657613236, -3.296219944818615577 ) ) ;
#19970=CARTESIAN_POINT ( 'NONE',  ( -2.696295709017761055, -5.948846446048906778, 4.997494388800372001E-16 ) ) ;
#19971=PLANE ( 'NONE',  #22603 ) ;
#19979=CARTESIAN_POINT ( 'NONE',  ( -3.458734125000000326, 1.432654583217640276, -0.3249999986344045411 ) ) ;
#19995=CARTESIAN_POINT ( 'NONE',  ( 3.458734125000000770, 4.235727675282972223E-16, -2.512499998634404097 ) ) ;
#20007=CARTESIAN_POINT ( 'NONE',  ( 1.656854249492380138, 4.000000000000000000, 1.112500002731187099 ) ) ;
#20024=ORIENTED_EDGE ( 'NONE', *, *, #14408, .F. ) ;
#20026=DIRECTION ( 'NONE',  ( -0.000000000000000000, -0.000000000000000000, 1.000000000000000000 ) ) ;
#20030=CARTESIAN_POINT ( 'NONE',  ( 2.445694354108820523, -2.445694354108820079, 5.112500001365595459 ) ) ;
#20031=ADVANCED_FACE ( 'NONE', ( #14578 ), #5205, .T. ) ;
#20042=CARTESIAN_POINT ( 'NONE',  ( -1.432654583217641164, -3.458734125000000326, 0.1750000013655959863 ) ) ;
#20044=CARTESIAN_POINT ( 'NONE',  ( -0.5303295852573156610, 7.199367570657603466, -3.296219944818624903 ) ) ;
#20049=CARTESIAN_POINT ( 'NONE',  ( 3.458734125000000326, 4.235727675282971730E-16, 1.237500001365595903 ) ) ;
#20080=CARTESIAN_POINT ( 'NONE',  ( 1.424327985892199999, -3.194194916198549006, 2.040000000000001812 ) ) ;
#20091=CARTESIAN_POINT ( 'NONE',  ( 1.432654583217642275, -3.458734124999999437, -1.949999998634404319 ) ) ;
#20109=CARTESIAN_POINT ( 'NONE',  ( -3.458734125000000770, 0.000000000000000000, -3.012499998634404541 ) ) ;
#20113=VERTEX_POINT ( 'NONE', #8257 ) ;
#20120=B_SPLINE_CURVE_WITH_KNOTS ( 'NONE', 3,
 ( #6901, #17795, #21241, #5209, #1246, #4981, #8584, #16355 ),
 .UNSPECIFIED., .F., .F.,
 ( 4, 2, 2, 4 ),
 ( 0.003797433802554436334, 0.004743183970586237024, 0.005688934138618036845, 0.007580434474681636489 ),
 .UNSPECIFIED. ) ;
#20138=ORIENTED_EDGE ( 'NONE', *, *, #17898, .F. ) ;
#20140=FACE_OUTER_BOUND ( 'NONE', #16799, .T. ) ;
#20144=CARTESIAN_POINT ( 'NONE',  ( -1.656854249492380804, 4.000000000000000000, -2.762499997268812457 ) ) ;
#20148=CARTESIAN_POINT ( 'NONE',  ( 4.000000000000000888, -1.656854249492379694, -2.262499999999998401 ) ) ;
#20155=CARTESIAN_POINT ( 'NONE',  ( -3.458734125000000770, 0.000000000000000000, -1.012499998634402543 ) ) ;
#20156=AXIS2_PLACEMENT_3D ( 'NONE', #18763, #2098, #9436 ) ;
#20164=CARTESIAN_POINT ( 'NONE',  ( 1.432654583217639832, 3.458734125000000326, -0.5749999986344046521 ) ) ;
#20176=ORIENTED_EDGE ( 'NONE', *, *, #4687, .T. ) ;
#20191=CARTESIAN_POINT ( 'NONE',  ( -6.500000000000000000, -3.752776749732573247, -3.119443416399232394 ) ) ;
#20199=EDGE_CURVE ( 'NONE', #18467, #18845, #16289, .T. ) ;
#20237=CARTESIAN_POINT ( 'NONE',  ( -4.000000000000000000, -1.656854249492383246, 5.362500000000002487 ) ) ;
#20247=CONICAL_SURFACE ( 'NONE', #6880, 6.500000000000000888, 1.047197551196596521 ) ;
#20270=EDGE_LOOP ( 'NONE', ( #9149, #7136, #13719 ) ) ;
#20273=CARTESIAN_POINT ( 'NONE',  ( -2.445694354108820523, 2.445694354108820523, 4.612500001365595459 ) ) ;
#20281=B_SPLINE_CURVE_WITH_KNOTS ( 'NONE', 3,
 ( #2975, #11653, #715, #22632, #13911, #4781 ),
 .UNSPECIFIED., .F., .F.,
 ( 4, 2, 4 ),
 ( 0.01049192114530184475, 0.01239128608052813933, 0.01429065101575443392 ),
 .UNSPECIFIED. ) ;
#20283=CARTESIAN_POINT ( 'NONE',  ( -2.445694354108820523, 2.445694354108820523, 0.8625000013655955700 ) ) ;
#20289=CARTESIAN_POINT ( 'NONE',  ( -2.445694354108820523, 2.445694354108820523, 0.6125000013655953479 ) ) ;
#20299=EDGE_CURVE ( 'NONE', #21072, #13238, #4809, .T. ) ;
#20310=CARTESIAN_POINT ( 'NONE',  ( 6.499999999999999112, -3.752776749732574135, -3.119443416399232394 ) ) ;
#20315=CARTESIAN_POINT ( 'NONE',  ( 2.486305999565482150, -2.591796431245380727, 2.040000000000000480 ) ) ;
#20317=CARTESIAN_POINT ( 'NONE',  ( -2.149474931388144050, -6.264553569211847694, -0.05533025579362477187 ) ) ;
#20319=CARTESIAN_POINT ( 'NONE',  ( -0.5303295852573153280, 7.199367570657603466, -0.4037800551813762739 ) ) ;
#20323=EDGE_CURVE ( 'NONE', #844, #7387, #12917, .T. ) ;
#20330=CARTESIAN_POINT ( 'NONE',  ( -4.000000000000000888, 1.656854249492380582, -2.762499999999997069 ) ) ;
#20333=EDGE_LOOP ( 'NONE', ( #15868, #17817, #19632 ) ) ;
#20349=CARTESIAN_POINT ( 'NONE',  ( -3.458734125000000770, 1.432654583217640498, -1.074999998634403209 ) ) ;
#20350=CARTESIAN_POINT ( 'NONE',  ( -4.000000000000000000, 0.000000000000000000, 4.299999999999999822 ) ) ;
#20368=ADVANCED_FACE ( 'NONE', ( #18960 ), #9761, .T. ) ;
#20384=DIRECTION ( 'NONE',  ( 1.000000000000000000, 0.000000000000000000, 0.000000000000000000 ) ) ;
#20387=CARTESIAN_POINT ( 'NONE',  ( 2.828427124746190735, -2.828427124746189847, -3.199999997268812901 ) ) ;
#20399=CARTESIAN_POINT ( 'NONE',  ( 2.445694354108820079, 2.445694354108820523, -0.3874999986344038194 ) ) ;
#20402=EDGE_CURVE ( 'NONE', #8785, #1632, #9738, .T. ) ;
#20405=CARTESIAN_POINT ( 'NONE',  ( -3.458734125000000326, 1.432654583217640276, -3.324999998634403209 ) ) ;
#20410=ORIENTED_EDGE ( 'NONE', *, *, #147, .T. ) ;
#20430=( BOUNDED_CURVE ( )  B_SPLINE_CURVE ( 2, ( #13998, #16149, #21259, #14121, #12213, #19483, #5113, #3082, #17704 ),
 .UNSPECIFIED., .F., .F. ) 
 B_SPLINE_CURVE_WITH_KNOTS ( ( 3, 2, 2, 2, 3 ),
 ( 0.7500000000000000000, 0.7624999999999999556, 0.7750000000000000222, 0.7874999999999999778, 0.8000000000000000444 ),
 .UNSPECIFIED. ) 
 CURVE ( )  GEOMETRIC_REPRESENTATION_ITEM ( )  RATIONAL_B_SPLINE_CURVE ( ( 1.000000000000000000, 0.9238795325112867385, 1.000000000000000000, 0.9238795325112867385, 1.000000000000000000, 0.9238795325112867385, 1.000000000000000000, 0.9238795325112867385, 1.000000000000000000 ) ) 
 REPRESENTATION_ITEM ( '' )  );
#20442=DIRECTION ( 'NONE',  ( 1.000000000000000000, 0.000000000000000000, 0.000000000000000000 ) ) ;
#20452=VERTEX_POINT ( 'NONE', #12642 ) ;
#20457=CARTESIAN_POINT ( 'NONE',  ( -3.803704290982251379, 5.309483803148795644, -3.700000000000004619 ) ) ;
#20470=CARTESIAN_POINT ( 'NONE',  ( -2.445694354108820523, 2.445694354108820523, -1.137499998634402765 ) ) ;
#20471=CARTESIAN_POINT ( 'NONE',  ( -2.828427124746190291, 2.828427124746190291, 0.1750000000000015432 ) ) ;
#20486=CARTESIAN_POINT ( 'NONE',  ( -1.656854249492380582, 4.000000000000000000, 1.237500002731187099 ) ) ;
#20500=CARTESIAN_POINT ( 'NONE',  ( -2.117863837641485618E-16, 3.458734125000000770, 5.737500001365596347 ) ) ;
#20509=( LENGTH_UNIT ( ) NAMED_UNIT ( * ) SI_UNIT ( .MILLI., .METRE. ) );
#20510=CARTESIAN_POINT ( 'NONE',  ( -1.432654583217640276, 3.458734125000000326, 3.550000001365595459 ) ) ;
#20511=CARTESIAN_POINT ( 'NONE',  ( 2.828427124746189847, 2.828427124746190291, 1.925000000000001377 ) ) ;
#20519=CARTESIAN_POINT ( 'NONE',  ( 3.458734125000000770, 4.235727675282972223E-16, -0.5124999986344038749 ) ) ;
#20525=CARTESIAN_POINT ( 'NONE',  ( 3.458734125000001214, -1.432654583217639610, 4.425000001365595459 ) ) ;
#20537=ORIENTED_EDGE ( 'NONE', *, *, #1401, .T. ) ;
#20540=( BOUNDED_CURVE ( )  B_SPLINE_CURVE ( 2, ( #22370, #16895, #3826, #7906, #18798, #12839, #3940, #18673, #5981 ),
 .UNSPECIFIED., .F., .F. ) 
 B_SPLINE_CURVE_WITH_KNOTS ( ( 3, 2, 2, 2, 3 ),
 ( 0.4500000000000000111, 0.4625000000000000222, 0.4749999999999999778, 0.4874999999999999889, 0.5000000000000000000 ),
 .UNSPECIFIED. ) 
 CURVE ( )  GEOMETRIC_REPRESENTATION_ITEM ( )  RATIONAL_B_SPLINE_CURVE ( ( 1.000000000000000000, 0.9238795325112867385, 1.000000000000000000, 0.9238795325112867385, 1.000000000000000000, 0.9238795325112867385, 1.000000000000000000, 0.9238795325112867385, 1.000000000000000000 ) ) 
 REPRESENTATION_ITEM ( '' )  );
#20551=VERTEX_POINT ( 'NONE', #16558 ) ;
#20571=CARTESIAN_POINT ( 'NONE',  ( -1.301042606982605321E-15, 7.505553499465137612, -0.5805565836007695601 ) ) ;
#20580=CARTESIAN_POINT ( 'NONE',  ( -1.301042606982605321E-15, 7.505553499465137612, -3.119443416399232394 ) ) ;
#20591=AXIS2_PLACEMENT_3D ( 'NONE', #9224, #23690, #3454 ) ;
#20592=CARTESIAN_POINT ( 'NONE',  ( -3.458734125000000770, 0.000000000000000000, -2.012499998634403653 ) ) ;
#20593=CARTESIAN_POINT ( 'NONE',  ( 2.828427124746190735, -2.828427124746189847, 2.675000000000002043 ) ) ;
#20606=EDGE_CURVE ( 'NONE', #13210, #15511, #6370, .T. ) ;
#20610=AXIS2_PLACEMENT_3D ( 'NONE', #22599, #9448, #13521 ) ;
#20621=CARTESIAN_POINT ( 'NONE',  ( 2.445694354108820967, -2.445694354108820079, 2.362500001365596791 ) ) ;
#20631=CARTESIAN_POINT ( 'NONE',  ( -3.458734125000000326, 0.000000000000000000, 1.737500001365596347 ) ) ;
#20654=CARTESIAN_POINT ( 'NONE',  ( -2.445694354108820523, 2.445694354108820523, 4.862500001365595459 ) ) ;
#20661=CARTESIAN_POINT ( 'NONE',  ( 4.000000000000000888, -1.656854249492379694, 4.862500002731188431 ) ) ;
#20666=CARTESIAN_POINT ( 'NONE',  ( 0.000000000000000000, 0.000000000000000000, 9.480888224575631185 ) ) ;
#20675=ORIENTED_EDGE ( 'NONE', *, *, #6433, .F. ) ;
#20694=ORIENTED_EDGE ( 'NONE', *, *, #23119, .T. ) ;
#20698=CARTESIAN_POINT ( 'NONE',  ( -6.500000000000000000, 3.752776749732573247, -3.119443416399232394 ) ) ;
#20712=CARTESIAN_POINT ( 'NONE',  ( 7.347880794884118750E-16, -4.000000000000000000, -0.4499999999999972911 ) ) ;
#20713=CARTESIAN_POINT ( 'NONE',  ( -1.656854249492381248, -3.999999999999999112, -3.387499997268812901 ) ) ;
#20716=ORIENTED_EDGE ( 'NONE', *, *, #20299, .T. ) ;
#20735=CARTESIAN_POINT ( 'NONE',  ( -3.458734125000000770, 0.000000000000000000, 2.987500001365597235 ) ) ;
#20736=EDGE_CURVE ( 'NONE', #6042, #9739, #22711, .T. ) ;
#20745=CARTESIAN_POINT ( 'NONE',  ( -2.445694354108819635, -2.445694354108820523, 2.862500001365597235 ) ) ;
#20747=CARTESIAN_POINT ( 'NONE',  ( -2.117863837641485618E-16, 3.458734125000000326, 1.487500001365596125 ) ) ;
#20748=ORIENTED_EDGE ( 'NONE', *, *, #5092, .T. ) ;
#20752=ORIENTED_EDGE ( 'NONE', *, *, #15650, .T. ) ;
#20761=EDGE_CURVE ( 'NONE', #8065, #15511, #6249, .T. ) ;
#20766=CARTESIAN_POINT ( 'NONE',  ( -2.117863837641485618E-16, 3.458734125000000770, 3.737500001365594571 ) ) ;
#20773=CARTESIAN_POINT ( 'NONE',  ( 7.347880794884118750E-16, -4.000000000000000000, 2.675000002731188875 ) ) ;
#20809=EDGE_LOOP ( 'NONE', ( #6520, #4167, #20752, #18488, #15778, #1077, #21019, #5560, #16858 ) ) ;
#20826=EDGE_LOOP ( 'NONE', ( #19749, #10300, #9320, #8674, #10749, #2479, #18320, #5110, #20138, #18671, #22817, #20024, #5748, #9126 ) ) ;
#20827=CARTESIAN_POINT ( 'NONE',  ( -4.000000000000000000, -1.656854249492383246, 2.362500000000002043 ) ) ;
#20837=CARTESIAN_POINT ( 'NONE',  ( -1.656854249492380582, 4.000000000000000000, -1.762499997268811569 ) ) ;
#20850=CARTESIAN_POINT ( 'NONE',  ( 6.353591512924457348E-16, -3.458734125000000770, 2.237500001365596791 ) ) ;
#20856=ORIENTED_EDGE ( 'NONE', *, *, #12301, .T. ) ;
#20860=CARTESIAN_POINT ( 'NONE',  ( 3.458734125000000326, 1.432654583217640498, 0.3000000013655960696 ) ) ;
#20861=CARTESIAN_POINT ( 'NONE',  ( -2.445694354108820523, 2.445694354108820523, 0.6125000013655953479 ) ) ;
#20868=CARTESIAN_POINT ( 'NONE',  ( -3.458734125000000770, 1.432654583217640498, -3.074999998634403209 ) ) ;
#20876=CARTESIAN_POINT ( 'NONE',  ( 3.458734125000000326, 4.235727675282971730E-16, -2.762499998634404097 ) ) ;
#20891=DIRECTION ( 'NONE',  ( -0.000000000000000000, -0.000000000000000000, 1.000000000000000000 ) ) ;
#20916=CARTESIAN_POINT ( 'NONE',  ( -6.500000000000000000, -3.752776749732573247, -0.5805565836007695601 ) ) ;
#20938=CARTESIAN_POINT ( 'NONE',  ( 4.000000000000000888, -1.656854249492379694, -0.2624999999999966804 ) ) ;
#20945=ORIENTED_EDGE ( 'NONE', *, *, #13484, .T. ) ;
#20949=ORIENTED_EDGE ( 'NONE', *, *, #11790, .F. ) ;
#20963=AXIS2_PLACEMENT_3D ( 'NONE', #5951, #20891, #18991 ) ;
#20964=CARTESIAN_POINT ( 'NONE',  ( 2.445694354108820079, 2.445694354108820523, 3.612500001365598123 ) ) ;
#20973=CARTESIAN_POINT ( 'NONE',  ( -3.458734125000000326, 0.000000000000000000, 0.7375000013655954589 ) ) ;
#20975=CARTESIAN_POINT ( 'NONE',  ( 1.432654583217642053, -3.458734124999999437, -0.9499999986344030978 ) ) ;
#20993=CIRCLE ( 'NONE', #10725, 6.500000000000000888 ) ;
#20996=CARTESIAN_POINT ( 'NONE',  ( 2.445694354108820967, -2.445694354108820079, 3.362500001365597679 ) ) ;
#21007=CARTESIAN_POINT ( 'NONE',  ( -1.656854249492381248, -3.999999999999999112, 3.612500002731187099 ) ) ;
#21017=VECTOR ( 'NONE', #9148, 1000.000000000000000 ) ;
#21019=ORIENTED_EDGE ( 'NONE', *, *, #8502, .F. ) ;
#21023=CARTESIAN_POINT ( 'NONE',  ( -3.250000000000004885, -5.629165124598848990, -3.700000000000000178 ) ) ;
#21041=CARTESIAN_POINT ( 'NONE',  ( -4.000000000000000888, 1.656854249492380582, 1.237500000000000488 ) ) ;
#21056=FACE_OUTER_BOUND ( 'NONE', #15509, .T. ) ;
#21058=CARTESIAN_POINT ( 'NONE',  ( 1.656854249492380360, 4.000000000000000000, -2.012499999999997957 ) ) ;
#21064=EDGE_LOOP ( 'NONE', ( #11304, #7704, #10830 ) ) ;
#21070=EDGE_LOOP ( 'NONE', ( #20694, #16497, #2455, #9632, #16128, #10199 ) ) ;
#21072=VERTEX_POINT ( 'NONE', #18670 ) ;
#21077=CARTESIAN_POINT ( 'NONE',  ( -2.449293598294706907E-16, 4.000000000000000000, -0.8249999972688125682 ) ) ;
#21084=CARTESIAN_POINT ( 'NONE',  ( -2.117863837641485618E-16, 3.458734125000000770, 0.7375000013655954589 ) ) ;
#21095=CARTESIAN_POINT ( 'NONE',  ( -2.445694354108820523, 2.445694354108820523, 1.612500001365596125 ) ) ;
#21103=CARTESIAN_POINT ( 'NONE',  ( -1.432654583217641164, -3.458734125000000326, -2.824999998634404541 ) ) ;
#21111=CARTESIAN_POINT ( 'NONE',  ( -3.458734125000000770, 1.432654583217640498, -0.07499999863440427739 ) ) ;
#21118=CARTESIAN_POINT ( 'NONE',  ( 1.656854249492380138, 4.000000000000000000, -2.012499999999998401 ) ) ;
#21123=CARTESIAN_POINT ( 'NONE',  ( -2.828427124746190291, 2.828427124746190291, 2.300000002731188431 ) ) ;
#21125=B_SPLINE_CURVE_WITH_KNOTS ( 'NONE', 3,
 ( #11374, #5487, #14853, #16398, #22108, #5728, #21765, #14501, #13060, #4044, #12822, #18652, #7658, #14981, #2241, #7186, #20315, #13169, #16285, #20080, #3680 ),
 .UNSPECIFIED., .F., .F.,
 ( 4, 2, 2, 2, 2, 2, 1, 2, 2, 2, 4 ),
 ( 0.000000000000000000, 0.0009109962461224923582, 0.001821992492244984066, 0.002732988738367476099, 0.003643984984489967698, 0.004099483107551214582, 0.004554981230612460165, 0.005010479353673706615, 0.005465977476734953065, 0.006376973722857446833, 0.007287969968979940601 ),
 .UNSPECIFIED. ) ;
#21127=CARTESIAN_POINT ( 'NONE',  ( 7.347880794884118750E-16, -4.000000000000000000, 1.675000002731187987 ) ) ;
#21136=DIRECTION ( 'NONE',  ( -0.000000000000000000, -0.000000000000000000, 1.000000000000000000 ) ) ;
#21138=CARTESIAN_POINT ( 'NONE',  ( -1.432654583217640276, 3.458734125000000326, 2.550000001365598123 ) ) ;
#21146=ORIENTED_EDGE ( 'NONE', *, *, #22504, .F. ) ;
#21170=CARTESIAN_POINT ( 'NONE',  ( 1.656854249492380360, 4.000000000000000000, -1.012499999999997513 ) ) ;
#21172=LINE ( 'NONE', #10571, #12022 ) ;
#21173=CARTESIAN_POINT ( 'NONE',  ( -1.656854249492380582, 4.000000000000000000, -0.8874999999999971800 ) ) ;
#21184=EDGE_CURVE ( 'NONE', #7010, #8065, #13722, .T. ) ;
#21190=AXIS2_PLACEMENT_3D ( 'NONE', #19378, #4779, #19617 ) ;
#21192=EDGE_CURVE ( 'NONE', #10634, #12600, #4691, .T. ) ;
#21194=EDGE_CURVE ( 'NONE', #4306, #21201, #10704, .T. ) ;
#21196=CARTESIAN_POINT ( 'NONE',  ( 3.458734125000001214, -1.432654583217639610, -1.574999998634403875 ) ) ;
#21200=DIRECTION ( 'NONE',  ( -0.000000000000000000, -0.000000000000000000, 1.000000000000000000 ) ) ;
#21201=VERTEX_POINT ( 'NONE', #13303 ) ;
#21206=CARTESIAN_POINT ( 'NONE',  ( -1.432654583217640942, -3.458734124999999882, 1.925000001365597457 ) ) ;
#21213=ORIENTED_EDGE ( 'NONE', *, *, #13484, .F. ) ;
#21228=CARTESIAN_POINT ( 'NONE',  ( -3.458734125000000326, -1.432654583217642497, 3.050000001365598568 ) ) ;
#21232=VERTEX_POINT ( 'NONE', #2730 ) ;
#21237=CARTESIAN_POINT ( 'NONE',  ( 4.000000000000000000, 4.898587196589412829E-16, 0.9250000027311873207 ) ) ;
#21241=CARTESIAN_POINT ( 'NONE',  ( 2.697128823393878605, -5.948365447239590154, -0.01372220897662065377 ) ) ;
#21252=CARTESIAN_POINT ( 'NONE',  ( 2.445694354108820523, -2.445694354108820079, 4.112500001365594571 ) ) ;
#21258=DIRECTION ( 'NONE',  ( 0.000000000000000000, -0.000000000000000000, 1.000000000000000000 ) ) ;
#21259=CARTESIAN_POINT ( 'NONE',  ( 2.828427124746190735, -2.828427124746189847, -1.324999999999997957 ) ) ;
#21283=CARTESIAN_POINT ( 'NONE',  ( -4.000000000000000000, -1.656854249492383246, -1.637499999999997735 ) ) ;
#21291=CARTESIAN_POINT ( 'NONE',  ( -6.499999999999999112, 2.531211054341939271, -0.2595069192555971571 ) ) ;
#21294=ORIENTED_EDGE ( 'NONE', *, *, #11725, .F. ) ;
#21309=CARTESIAN_POINT ( 'NONE',  ( -1.432654583217640498, 3.458734125000000770, -1.199999998634403431 ) ) ;
#21324=CARTESIAN_POINT ( 'NONE',  ( 2.445694354108820523, -2.445694354108820079, -1.887499998634403431 ) ) ;
#21344=CARTESIAN_POINT ( 'NONE',  ( 1.432654583217640276, 3.458734125000000770, 1.675000001365597235 ) ) ;
#21349=ORIENTED_EDGE ( 'NONE', *, *, #9854, .F. ) ;
#21354=CARTESIAN_POINT ( 'NONE',  ( -4.000000000000000888, 1.656854249492380804, 1.362500002731187321 ) ) ;
#21360=EDGE_LOOP ( 'NONE', ( #20945, #11612, #240, #15080, #155, #11034, #5390, #12156, #1728, #17812, #10723, #12775, #6486, #8417, #20176, #20748 ) ) ;
#21363=ADVANCED_FACE ( 'NONE', ( #12341 ), #10431, .F. ) ;
#21368=CARTESIAN_POINT ( 'NONE',  ( 4.000000000000000000, 4.898587196589412829E-16, 1.800000000000001155 ) ) ;
#21375=CARTESIAN_POINT ( 'NONE',  ( 2.445694354108820523, -2.445694354108820079, 2.112500001365596791 ) ) ;
#21381=CARTESIAN_POINT ( 'NONE',  ( -1.645496052585941671, 3.496231076593029119, 2.039999999999998259 ) ) ;
#21409=CARTESIAN_POINT ( 'NONE',  ( -6.500000000000000000, -3.752776749732572359, -3.700000000000000178 ) ) ;
#21412=CARTESIAN_POINT ( 'NONE',  ( -2.842195834095098572, 1.980645989956865138, -3.295601554149321988 ) ) ;
#21414=CARTESIAN_POINT ( 'NONE',  ( -4.000000000000000000, 0.000000000000000000, 0.4250000027311868211 ) ) ;
#21426=AXIS2_PLACEMENT_3D ( 'NONE', #18325, #5153, #16309 ) ;
#21432=CARTESIAN_POINT ( 'NONE',  ( 0.000000000000000000, 0.000000000000000000, 9.480888224575631185 ) ) ;
#21434=CARTESIAN_POINT ( 'NONE',  ( -2.117863837641485618E-16, 3.458734125000000770, 1.737500001365596347 ) ) ;
#21447=CARTESIAN_POINT ( 'NONE',  ( 1.432654583217639832, 3.458734125000000326, -2.574999998634404541 ) ) ;
#21452=VERTEX_POINT ( 'NONE', #5120 ) ;
#21464=CARTESIAN_POINT ( 'NONE',  ( 2.445694354108820967, -2.445694354108820079, 1.362500001365595903 ) ) ;
#21468=ORIENTED_EDGE ( 'NONE', *, *, #1603, .T. ) ;
#21474=CARTESIAN_POINT ( 'NONE',  ( 1.656854249492380360, 4.000000000000000000, -0.8874999972688129013 ) ) ;
#21492=CARTESIAN_POINT ( 'NONE',  ( -2.445694354108819635, -2.445694354108820523, 3.862500001365594571 ) ) ;
#21496=B_SPLINE_CURVE_WITH_KNOTS ( 'NONE', 3,
 ( #10502, #19675, #17781, #9174, #8817, #19919, #23155, #21831, #7127, #12300, #1474, #9050, #3156, #5434, #1595, #1354, #3281, #16115 ),
 .UNSPECIFIED., .F., .F.,
 ( 4, 2, 2, 2, 2, 2, 2, 2, 4 ),
 ( 0.000000000000000000, 0.0006826094070889694504, 0.001365218814177938901, 0.002047828221266908676, 0.002730437628355877801, 0.003413047035444848228, 0.004095656442533819087, 0.004778265849622789080, 0.005460875256711760807 ),
 .UNSPECIFIED. ) ;
#21504=EDGE_LOOP ( 'NONE', ( #23561, #17385, #7994, #12785 ) ) ;
#21522=CARTESIAN_POINT ( 'NONE',  ( 4.000000000000000000, 4.898587196589412829E-16, -1.074999997268812679 ) ) ;
#21527=AXIS2_PLACEMENT_3D ( 'NONE', #9235, #21648, #14625 ) ;
#21530=CARTESIAN_POINT ( 'NONE',  ( -3.298587526675563097, 1.112609898547286980, -3.295601554149322876 ) ) ;
#21536=CARTESIAN_POINT ( 'NONE',  ( -3.458734125000000326, 1.432654583217640276, -2.324999998634404097 ) ) ;
#21545=DIRECTION ( 'NONE',  ( -0.8660254037844382635, 0.5000000000000006661, 0.000000000000000000 ) ) ;
#21552=CARTESIAN_POINT ( 'NONE',  ( 2.445694354108820967, -2.445694354108820079, 0.3625000013655968467 ) ) ;
#21563=CARTESIAN_POINT ( 'NONE',  ( 2.445694354108820079, 2.445694354108820523, -1.637499998634403209 ) ) ;
#21564=ORIENTED_EDGE ( 'NONE', *, *, #1168, .F. ) ;
#21578=CARTESIAN_POINT ( 'NONE',  ( 4.000000000000000000, 0.000000000000000000, 19.04999999999996874 ) ) ;
#21580=CARTESIAN_POINT ( 'NONE',  ( -3.458734125000000326, -1.432654583217642497, -2.949999998634404985 ) ) ;
#21591=CARTESIAN_POINT ( 'NONE',  ( 4.000000000000000888, -1.656854249492379694, 1.862500002731187765 ) ) ;
#21612=CARTESIAN_POINT ( 'NONE',  ( -3.458734125000000326, 0.000000000000000000, 3.737500001365594571 ) ) ;
#21621=CARTESIAN_POINT ( 'NONE',  ( -6.500000000000002665, 1.277696550142690235, -3.643982548855206449 ) ) ;
#21627=EDGE_CURVE ( 'NONE', #10924, #15256, #6467, .T. ) ;
#21645=CARTESIAN_POINT ( 'NONE',  ( -1.647987302177966740E-14, -7.505553499465137612, -0.5805565836007695601 ) ) ;
#21648=DIRECTION ( 'NONE',  ( -0.000000000000000000, -0.000000000000000000, 1.000000000000000000 ) ) ;
#21650=EDGE_CURVE ( 'NONE', #7387, #15758, #8406, .T. ) ;
#21655=CARTESIAN_POINT ( 'NONE',  ( 2.445694354108820523, -2.445694354108820079, -2.887499998634404097 ) ) ;
#21661=EDGE_LOOP ( 'NONE', ( #5893, #11241, #15442 ) ) ;
#21668=CARTESIAN_POINT ( 'NONE',  ( 0.000000000000000000, 0.000000000000000000, 19.04999999999996874 ) ) ;
#21674=AXIS2_PLACEMENT_3D ( 'NONE', #9017, #6, #12620 ) ;
#21675=CARTESIAN_POINT ( 'NONE',  ( -2.445694354108820523, 2.445694354108820523, -3.137499998634402765 ) ) ;
#21681=CIRCLE ( 'NONE', #10253, 4.714285714285714413 ) ;
#21696=ADVANCED_FACE ( 'NONE', ( #6069 ), #2706, .F. ) ;
#21706=CARTESIAN_POINT ( 'NONE',  ( 1.432654583217642275, -3.458734124999999882, -1.699999998634404097 ) ) ;
#21713=CARTESIAN_POINT ( 'NONE',  ( 4.000000000000000888, -1.656854249492379694, 0.8625000027311868767 ) ) ;
#21719=CARTESIAN_POINT ( 'NONE',  ( -4.000000000000000888, 1.656854249492380582, -2.637499997268812013 ) ) ;
#21729=CARTESIAN_POINT ( 'NONE',  ( -3.250000000000004441, 5.629165124598849879, -3.700000000000000178 ) ) ;
#21733=CARTESIAN_POINT ( 'NONE',  ( 1.432654583217639832, 3.458734125000000326, 1.425000001365596791 ) ) ;
#21765=CARTESIAN_POINT ( 'NONE',  ( 3.820581514278380109, 0.3741733693073286959, 2.039999999999999591 ) ) ;
#21772=CARTESIAN_POINT ( 'NONE',  ( -2.117863837641483646E-16, 3.458734125000000770, -3.295601554149324208 ) ) ;
#21802=CARTESIAN_POINT ( 'NONE',  ( -3.458734125000000326, -1.432654583217642497, -2.949999998634404985 ) ) ;
#21820=LINE ( 'NONE', #30, #16734 ) ;
#21831=CARTESIAN_POINT ( 'NONE',  ( -1.101472369599993062, -3.286364942703593695, 2.039999999999997371 ) ) ;
#21838=EDGE_LOOP ( 'NONE', ( #8533, #17353, #10018 ) ) ;
#21840=CARTESIAN_POINT ( 'NONE',  ( 1.656854249492380360, 4.000000000000000000, -2.887499997268812457 ) ) ;
#21854=CARTESIAN_POINT ( 'NONE',  ( 2.445694354108820079, 2.445694354108820523, -1.637499998634403209 ) ) ;
#21862=ORIENTED_EDGE ( 'NONE', *, *, #20199, .T. ) ;
#21891=CARTESIAN_POINT ( 'NONE',  ( 2.445694354108820079, 2.445694354108820523, -1.637499998634403209 ) ) ;
#21909=B_SPLINE_CURVE_WITH_KNOTS ( 'NONE', 3,
 ( #20580, #9474, #6226, #352, #13310, #8037 ),
 .UNSPECIFIED., .F., .F.,
 ( 4, 2, 4 ),
 ( 2.380733003127974818E-07, 0.001898835937927380270, 0.003797433802554448044 ),
 .UNSPECIFIED. ) ;
#21910=CARTESIAN_POINT ( 'NONE',  ( -2.445694354108819635, -2.445694354108820967, -2.887499998634404097 ) ) ;
#21945=CARTESIAN_POINT ( 'NONE',  ( 7.347880794884118750E-16, -4.000000000000000000, -3.324999997268812901 ) ) ;
#21949=CARTESIAN_POINT ( 'NONE',  ( -1.656854249492381248, -3.999999999999999112, -2.512499999999998845 ) ) ;
#21955=CARTESIAN_POINT ( 'NONE',  ( -3.270501301980698550, -1.125461230421587633, 2.040000000000001812 ) ) ;
#21964=CARTESIAN_POINT ( 'NONE',  ( -3.458734124999999882, -1.432654583217642497, -1.199999998634403431 ) ) ;
#21967=CARTESIAN_POINT ( 'NONE',  ( -2.828427124746190291, 2.828427124746190291, 0.1750000000000015432 ) ) ;
#21993=CARTESIAN_POINT ( 'NONE',  ( 1.876855952934447513, -6.421950209808290566, -3.593844378834461395 ) ) ;
#22018=CARTESIAN_POINT ( 'NONE',  ( -4.000000000000000000, 0.000000000000000000, -0.5749999972688123462 ) ) ;
#22023=CARTESIAN_POINT ( 'NONE',  ( 2.828427124746190735, -2.828427124746189847, 4.675000000000000711 ) ) ;
#22056=CARTESIAN_POINT ( 'NONE',  ( -3.458734125000000326, 0.000000000000000000, 5.737500001365596347 ) ) ;
#22066=( BOUNDED_SURFACE ( )  B_SPLINE_SURFACE ( 1, 2, ( 
 ( #11601, #6307, #789, #9914, #13508, #542, #895, #13394, #657, #20661, #12071, #11716, #22812, #2342, #17449, #17330, #7866, #4379, #18868, #15188, #13865, #2453, #9788, #22585, #17084, #17211, #13623, #7991, #8346, #21007, #4494, #19111, #11835, #18982, #4624, #11958, #15313, #6188, #2700, #10156, #8230, #15547, #6424, #22448, #20773, #13741, #4739, #15664, #6061, #22937, #21123, #6550, #23407, #5084, #3053, #10630, #19806, #21591, #18027, #8475, #3408, #15780, #17679, #1483, #5204, #21354, #16001, #6664, #17906, #14329, #5325, #23286, #21237, #21713, #10274, #14448, #23522, #7134, #13977, #17565, #1243, #12418, #4849, #12184, #8697, #19684, #16234, #17791, #8826, #12544, #14216, #15886, #10753, #1602, #1130, #16123, #1361, #19336, #23051, #6896, #7012, #21474, #2924, #19456, #8943, #10399, #8581, #19569, #23164, #6774, #14090, #4976, #12307, #3164, #10510, #3289, #13008, #9528, #22304, #406, #7259, #18484, #12777, #16826, #16349, #12887, #5556, #9293, #14688, #3526, #18374, #20144, #19926, #21840, #11210, #16470, #2191, #7733, #20387, #10972, #21945, #18136, #7491, #9058, #161, #2067, #14576, #47, #18248 ),
 ( #22056, #7381, #15046, #5442, #14807, #5674, #1716, #10859, #9408, #12670, #20030, #23645, #3993, #13127, #3633, #3748, #16698, #11089, #20273, #1833, #9183, #11334, #1954, #16582, #3877, #274, #7609, #14932, #22186, #5799, #18605, #4114, #4240, #9652, #11453, #20510, #13593, #7840, #2541, #4466, #6161, #18843, #2670, #11575, #2318, #11688, #20745, #11807, #13483, #15163, #16942, #22422, #7962, #11930, #17415, #2782, #519, #4593, #18957, #9886, #631, #6391, #15281, #18729, #20631, #5916, #22554, #6036, #9759, #760, #19078, #13362, #13244, #17178, #4351, #2428, #8092, #13711, #22783, #17301, #20973, #10122, #984, #15402, #22665, #17059, #6276, #20860, #10013, #865, #8200, #15514, #19197, #8638, #15938, #9241, #8885, #19979, #23218, #14631, #7200, #5034, #1546, #1414, #6830, #11032, #17847, #8756, #19746, #14275, #23468, #19867, #16062, #5501, #23352, #5264, #10335, #12365, #21891, #16179, #10690, #9007, #17964, #20091, #6958, #7075, #23588, #10810, #1663, #21536, #12832, #10575, #3582, #5144, #19627, #12608, #14392, #5388, #21655, #12485, #3225, #3348, #3471, #3692, #18316, #1898, #18082, #14154, #16299 ) ),
 .UNSPECIFIED., .F., .F., .F. ) 
 B_SPLINE_SURFACE_WITH_KNOTS ( ( 2, 2 ),
 ( 3, 2, 2, 2, 2, 2, 2, 2, 2, 2, 2, 2, 2, 2, 2, 2, 2, 2, 2, 2, 2, 2, 2, 2, 2, 2, 2, 2, 2, 2, 2, 2, 2, 2, 2, 2, 2, 2, 2, 2, 2, 2, 2, 2, 2, 2, 2, 2, 2, 2, 2, 2, 2, 2, 2, 2, 2, 2, 2, 2, 2, 2, 2, 2, 2, 2, 2, 2, 2, 2, 2, 2, 2, 2, 3 ),
 ( 0.000000000000000000, 1.000000000000000000 ),
 ( 0.000000000000000000, 0.01250000000000000069, 0.02500000000000000139, 0.03749999999999999861, 0.05000000000000000278, 0.06250000000000000000, 0.07499999999999999722, 0.08749999999999999445, 0.1000000000000000056, 0.1125000000000000028, 0.1250000000000000000, 0.1375000000000000111, 0.1499999999999999944, 0.1625000000000000056, 0.1749999999999999889, 0.1875000000000000000, 0.2000000000000000111, 0.2124999999999999944, 0.2250000000000000056, 0.2374999999999999889, 0.2500000000000000000, 0.2625000000000000111, 0.2750000000000000222, 0.2874999999999999778, 0.2999999999999999889, 0.3125000000000000000, 0.3250000000000000111, 0.3375000000000000222, 0.3499999999999999778, 0.3624999999999999889, 0.3750000000000000000, 0.3875000000000000111, 0.4000000000000000222, 0.4124999999999999778, 0.4249999999999999889, 0.4375000000000000000, 0.4500000000000000111, 0.4625000000000000222, 0.4749999999999999778, 0.4874999999999999889, 0.5000000000000000000, 0.5124999999999999556, 0.5250000000000000222, 0.5374999999999999778, 0.5500000000000000444, 0.5625000000000000000, 0.5749999999999999556, 0.5875000000000000222, 0.5999999999999999778, 0.6125000000000000444, 0.6250000000000000000, 0.6374999999999999556, 0.6500000000000000222, 0.6624999999999999778, 0.6750000000000000444, 0.6875000000000000000, 0.6999999999999999556, 0.7125000000000000222, 0.7249999999999999778, 0.7375000000000000444, 0.7500000000000000000, 0.7624999999999999556, 0.7750000000000000222, 0.7874999999999999778, 0.8000000000000000444, 0.8125000000000000000, 0.8249999999999999556, 0.8375000000000000222, 0.8499999999999999778, 0.8625000000000000444, 0.8750000000000000000, 0.8874999999999999556, 0.9000000000000000222, 0.9124999999999999778, 0.9250000000000000444 ),
 .UNSPECIFIED. ) 
 GEOMETRIC_REPRESENTATION_ITEM ( )  RATIONAL_B_SPLINE_SURFACE ( (
 ( 1.000000000000000000, 0.9238795325112867385, 1.000000000000000000, 0.9238795325112867385, 1.000000000000000000, 0.9238795325112867385, 1.000000000000000000, 0.9238795325112867385, 1.000000000000000000, 0.9238795325112867385, 1.000000000000000000, 0.9238795325112867385, 1.000000000000000000, 0.9238795325112867385, 1.000000000000000000, 0.9238795325112867385, 1.000000000000000000, 0.9238795325112867385, 1.000000000000000000, 0.9238795325112867385, 1.000000000000000000, 0.9238795325112867385, 1.000000000000000000, 0.9238795325112867385, 1.000000000000000000, 0.9238795325112867385, 1.000000000000000000, 0.9238795325112867385, 1.000000000000000000, 0.9238795325112867385, 1.000000000000000000, 0.9238795325112867385, 1.000000000000000000, 0.9238795325112867385, 1.000000000000000000, 0.9238795325112867385, 1.000000000000000000, 0.9238795325112867385, 1.000000000000000000, 0.9238795325112867385, 1.000000000000000000, 0.9238795325112867385, 1.000000000000000000, 0.9238795325112867385, 1.000000000000000000, 0.9238795325112867385, 1.000000000000000000, 0.9238795325112867385, 1.000000000000000000, 0.9238795325112867385, 1.000000000000000000, 0.9238795325112867385, 1.000000000000000000, 0.9238795325112867385, 1.000000000000000000, 0.9238795325112867385, 1.000000000000000000, 0.9238795325112867385, 1.000000000000000000, 0.9238795325112867385, 1.000000000000000000, 0.9238795325112867385, 1.000000000000000000, 0.9238795325112867385, 1.000000000000000000, 0.9238795325112867385, 1.000000000000000000, 0.9238795325112867385, 1.000000000000000000, 0.9238795325112867385, 1.000000000000000000, 0.9238795325112867385, 1.000000000000000000, 0.9238795325112867385, 1.000000000000000000, 0.9238795325112867385, 1.000000000000000000, 0.9238795325112867385, 1.000000000000000000, 0.9238795325112867385, 1.000000000000000000, 0.9238795325112867385, 1.000000000000000000, 0.9238795325112867385, 1.000000000000000000, 0.9238795325112867385, 1.000000000000000000, 0.9238795325112867385, 1.000000000000000000, 0.9238795325112867385, 1.000000000000000000, 0.9238795325112867385, 1.000000000000000000, 0.9238795325112867385, 1.000000000000000000, 0.9238795325112867385, 1.000000000000000000, 0.9238795325112867385, 1.000000000000000000, 0.9238795325112867385, 1.000000000000000000, 0.9238795325112867385, 1.000000000000000000, 0.9238795325112867385, 1.000000000000000000, 0.9238795325112867385, 1.000000000000000000, 0.9238795325112867385, 1.000000000000000000, 0.9238795325112867385, 1.000000000000000000, 0.9238795325112867385, 1.000000000000000000, 0.9238795325112867385, 1.000000000000000000, 0.9238795325112867385, 1.000000000000000000, 0.9238795325112867385, 1.000000000000000000, 0.9238795325112867385, 1.000000000000000000, 0.9238795325112867385, 1.000000000000000000, 0.9238795325112867385, 1.000000000000000000, 0.9238795325112867385, 1.000000000000000000, 0.9238795325112867385, 1.000000000000000000, 0.9238795325112867385, 1.000000000000000000, 0.9238795325112867385, 1.000000000000000000, 0.9238795325112867385, 1.000000000000000000, 0.9238795325112867385, 1.000000000000000000, 0.9238795325112867385, 1.000000000000000000, 0.9238795325112867385, 1.000000000000000000, 0.9238795325112867385, 1.000000000000000000, 0.9238795325112867385, 1.000000000000000000, 0.9238795325112867385, 1.000000000000000000, 0.9238795325112867385, 1.000000000000000000),
 ( 1.000000000000000000, 0.9238795325112867385, 1.000000000000000000, 0.9238795325112867385, 1.000000000000000000, 0.9238795325112867385, 1.000000000000000000, 0.9238795325112867385, 1.000000000000000000, 0.9238795325112867385, 1.000000000000000000, 0.9238795325112867385, 1.000000000000000000, 0.9238795325112867385, 1.000000000000000000, 0.9238795325112867385, 1.000000000000000000, 0.9238795325112867385, 1.000000000000000000, 0.9238795325112867385, 1.000000000000000000, 0.9238795325112867385, 1.000000000000000000, 0.9238795325112867385, 1.000000000000000000, 0.9238795325112867385, 1.000000000000000000, 0.9238795325112867385, 1.000000000000000000, 0.9238795325112867385, 1.000000000000000000, 0.9238795325112867385, 1.000000000000000000, 0.9238795325112867385, 1.000000000000000000, 0.9238795325112867385, 1.000000000000000000, 0.9238795325112867385, 1.000000000000000000, 0.9238795325112867385, 1.000000000000000000, 0.9238795325112867385, 1.000000000000000000, 0.9238795325112867385, 1.000000000000000000, 0.9238795325112867385, 1.000000000000000000, 0.9238795325112867385, 1.000000000000000000, 0.9238795325112867385, 1.000000000000000000, 0.9238795325112867385, 1.000000000000000000, 0.9238795325112867385, 1.000000000000000000, 0.9238795325112867385, 1.000000000000000000, 0.9238795325112867385, 1.000000000000000000, 0.9238795325112867385, 1.000000000000000000, 0.9238795325112867385, 1.000000000000000000, 0.9238795325112867385, 1.000000000000000000, 0.9238795325112867385, 1.000000000000000000, 0.9238795325112867385, 1.000000000000000000, 0.9238795325112867385, 1.000000000000000000, 0.9238795325112867385, 1.000000000000000000, 0.9238795325112867385, 1.000000000000000000, 0.9238795325112867385, 1.000000000000000000, 0.9238795325112867385, 1.000000000000000000, 0.9238795325112867385, 1.000000000000000000, 0.9238795325112867385, 1.000000000000000000, 0.9238795325112867385, 1.000000000000000000, 0.9238795325112867385, 1.000000000000000000, 0.9238795325112867385, 1.000000000000000000, 0.9238795325112867385, 1.000000000000000000, 0.9238795325112867385, 1.000000000000000000, 0.9238795325112867385, 1.000000000000000000, 0.9238795325112867385, 1.000000000000000000, 0.9238795325112867385, 1.000000000000000000, 0.9238795325112867385, 1.000000000000000000, 0.9238795325112867385, 1.000000000000000000, 0.9238795325112867385, 1.000000000000000000, 0.9238795325112867385, 1.000000000000000000, 0.9238795325112867385, 1.000000000000000000, 0.9238795325112867385, 1.000000000000000000, 0.9238795325112867385, 1.000000000000000000, 0.9238795325112867385, 1.000000000000000000, 0.9238795325112867385, 1.000000000000000000, 0.9238795325112867385, 1.000000000000000000, 0.9238795325112867385, 1.000000000000000000, 0.9238795325112867385, 1.000000000000000000, 0.9238795325112867385, 1.000000000000000000, 0.9238795325112867385, 1.000000000000000000, 0.9238795325112867385, 1.000000000000000000, 0.9238795325112867385, 1.000000000000000000, 0.9238795325112867385, 1.000000000000000000, 0.9238795325112867385, 1.000000000000000000, 0.9238795325112867385, 1.000000000000000000, 0.9238795325112867385, 1.000000000000000000, 0.9238795325112867385, 1.000000000000000000, 0.9238795325112867385, 1.000000000000000000, 0.9238795325112867385, 1.000000000000000000, 0.9238795325112867385, 1.000000000000000000, 0.9238795325112867385, 1.000000000000000000) ) ) 
 REPRESENTATION_ITEM ( '' )  SURFACE ( )  );
#22067=CARTESIAN_POINT ( 'NONE',  ( 2.445694354108820079, 2.445694354108820523, 1.612500001365596125 ) ) ;
#22076=CARTESIAN_POINT ( 'NONE',  ( -2.445694354108819635, -2.445694354108820523, -0.1374999986344035974 ) ) ;
#22091=AXIS2_PLACEMENT_3D ( 'NONE', #19200, #13952, #15864 ) ;
#22108=CARTESIAN_POINT ( 'NONE',  ( 3.689044737729619161, 1.278153343311797085, 2.040000000000004921 ) ) ;
#22119=ADVANCED_FACE ( 'NONE', ( #17646 ), #12032, .F. ) ;
#22139=ORIENTED_EDGE ( 'NONE', *, *, #22978, .T. ) ;
#22147=CARTESIAN_POINT ( 'NONE',  ( -3.458734125000000770, 1.432654583217640498, -3.074999998634403209 ) ) ;
#22148=CARTESIAN_POINT ( 'NONE',  ( 1.656854249492383024, -3.999999999999999112, 4.612500000000001599 ) ) ;
#22152=ORIENTED_EDGE ( 'NONE', *, *, #5326, .T. ) ;
#22175=CARTESIAN_POINT ( 'NONE',  ( -3.458734125000000770, 1.432654583217640498, 5.925000001365596347 ) ) ;
#22183=ORIENTED_EDGE ( 'NONE', *, *, #15076, .F. ) ;
#22186=CARTESIAN_POINT ( 'NONE',  ( 6.353591512924457348E-16, -3.458734125000000326, 3.987500001365595015 ) ) ;
#22187=CARTESIAN_POINT ( 'NONE',  ( 0.000000000000000000, 0.000000000000000000, 3.059999999999998277 ) ) ;
#22191=CARTESIAN_POINT ( 'NONE',  ( -2.449293598294706907E-16, 4.000000000000000000, -2.824999997268812457 ) ) ;
#22196=CARTESIAN_POINT ( 'NONE',  ( 1.432654583217640276, 3.458734125000000770, 0.6750000013655963471 ) ) ;
#22203=CARTESIAN_POINT ( 'NONE',  ( 1.432654583217642275, -3.458734124999999437, 0.05000000136559582670 ) ) ;
#22212=VECTOR ( 'NONE', #14737, 1000.000000000000000 ) ;
#22216=( BOUNDED_CURVE ( )  B_SPLINE_CURVE ( 2, ( #11908, #2761, #10104, #22885, #21077, #10222, #12134, #2994, #19876 ),
 .UNSPECIFIED., .F., .F. ) 
 B_SPLINE_CURVE_WITH_KNOTS ( ( 3, 2, 2, 2, 3 ),
 ( 0.5999999999999999778, 0.6125000000000000444, 0.6250000000000000000, 0.6374999999999999556, 0.6500000000000000222 ),
 .UNSPECIFIED. ) 
 CURVE ( )  GEOMETRIC_REPRESENTATION_ITEM ( )  RATIONAL_B_SPLINE_CURVE ( ( 1.000000000000000000, 0.9238795325112867385, 1.000000000000000000, 0.9238795325112867385, 1.000000000000000000, 0.9238795325112867385, 1.000000000000000000, 0.9238795325112867385, 1.000000000000000000 ) ) 
 REPRESENTATION_ITEM ( '' )  );
#22229=ORIENTED_EDGE ( 'NONE', *, *, #16249, .F. ) ;
#22269=CARTESIAN_POINT ( 'NONE',  ( -1.656854249492380804, 4.000000000000000000, 1.112500000000000711 ) ) ;
#22270=CARTESIAN_POINT ( 'NONE',  ( 1.656854249492383024, -3.999999999999999112, -3.262499997268812901 ) ) ;
#22279=CARTESIAN_POINT ( 'NONE',  ( 2.828427124746189847, 2.828427124746190291, 1.050000002731187321 ) ) ;
#22285=AXIS2_PLACEMENT_3D ( 'NONE', #7249, #17897, #8934 ) ;
#22291=DIRECTION ( 'NONE',  ( 0.5000000000000004441, -0.8660254037844383745, 0.000000000000000000 ) ) ;
#22293=DIRECTION ( 'NONE',  ( 1.000000000000000000, 0.000000000000000000, 0.000000000000000000 ) ) ;
#22304=CARTESIAN_POINT ( 'NONE',  ( 2.828427124746189847, 2.828427124746190291, -1.949999997268811791 ) ) ;
#22309=CARTESIAN_POINT ( 'NONE',  ( -2.338817011410299154E-16, 3.819578041666666923, -3.054166666211466374 ) ) ;
#22314=CARTESIAN_POINT ( 'NONE',  ( 1.432654583217642053, -3.458734124999999882, -0.6999999986344028757 ) ) ;
#22320=CARTESIAN_POINT ( 'NONE',  ( 3.458734125000000770, 4.235727675282972223E-16, 5.487500001365596347 ) ) ;
#22353=CARTESIAN_POINT ( 'NONE',  ( -1.656854249492381248, -3.999999999999999112, 0.4875000000000020983 ) ) ;
#22370=CARTESIAN_POINT ( 'NONE',  ( 4.000000000000000000, 4.898587196589412829E-16, 1.800000000000001155 ) ) ;
#22373=B_SPLINE_CURVE_WITH_KNOTS ( 'NONE', 3,
 ( #3639, #22309, #5679, #13014 ),
 .UNSPECIFIED., .F., .F.,
 ( 4, 4 ),
 ( 0.000000000000000000, 1.000000000000000000 ),
 .UNSPECIFIED. ) ;
#22386=CARTESIAN_POINT ( 'NONE',  ( 3.458734125000000770, 1.432654583217640498, -1.449999998634403653 ) ) ;
#22387=CARTESIAN_POINT ( 'NONE',  ( -2.449293598294706907E-16, 4.000000000000000000, 2.050000000000001599 ) ) ;
#22402=CARTESIAN_POINT ( 'NONE',  ( 4.000000000000000000, 4.898587196589412829E-16, -2.074999997268812013 ) ) ;
#22414=CARTESIAN_POINT ( 'NONE',  ( 1.432654583217642275, -3.458734124999999882, 5.300000001365596347 ) ) ;
#22422=CARTESIAN_POINT ( 'NONE',  ( -1.432654583217640276, 3.458734125000000326, 2.550000001365598123 ) ) ;
#22431=CIRCLE ( 'NONE', #21674, 5.479999999999998650 ) ;
#22433=CARTESIAN_POINT ( 'NONE',  ( -1.432654583217640498, 3.458734125000000770, -2.199999998634404097 ) ) ;
#22437=CONICAL_SURFACE ( 'NONE', #5237, 4.000000000000000000, 0.9599310885968780349 ) ;
#22440=CARTESIAN_POINT ( 'NONE',  ( -3.458734125000000770, 1.432654583217640498, 3.925000001365594127 ) ) ;
#22448=CARTESIAN_POINT ( 'NONE',  ( 1.656854249492383024, -3.999999999999999112, 2.737500002731188431 ) ) ;
#22455=CARTESIAN_POINT ( 'NONE',  ( 4.000000000000000000, 4.898587196589412829E-16, 1.925000002731188209 ) ) ;
#22467=CARTESIAN_POINT ( 'NONE',  ( 4.000000000000000000, 1.656854249492381248, -0.01249999726881388488 ) ) ;
#22473=AXIS2_PLACEMENT_3D ( 'NONE', #19306, #12155, #19423 ) ;
#22487=CARTESIAN_POINT ( 'NONE',  ( 4.000000000000000000, 4.898587196589412829E-16, 0.8000000000000020428 ) ) ;
#22495=FACE_OUTER_BOUND ( 'NONE', #3627, .T. ) ;
#22501=CARTESIAN_POINT ( 'NONE',  ( 5.969670414742682674, 4.058962678540098956, -0.4037800551813739425 ) ) ;
#22504=EDGE_CURVE ( 'NONE', #8139, #7387, #782, .T. ) ;
#22510=CARTESIAN_POINT ( 'NONE',  ( -4.000000000000000000, -1.656854249492383246, 3.362500000000005151 ) ) ;
#22535=B_SPLINE_CURVE_WITH_KNOTS ( 'NONE', 3,
 ( #5111, #5226, #3436, #10777, #23071, #6682, #19481, #3080, #3311, #10422, #15908, #8719, #17702, #1265, #23185, #6797, #16027, #14118, #21381, #3190, #23315, #6924, #16493, #2093 ),
 .UNSPECIFIED., .F., .F.,
 ( 4, 2, 2, 2, 2, 2, 2, 2, 2, 2, 2, 4 ),
 ( 0.000000000000000000, 0.0009154863746717545282, 0.001373229562007631738, 0.001830972749343509056, 0.002746459124015263042, 0.003204202311351139927, 0.003661945498687016378, 0.004577431873358769714, 0.005035175060694646598, 0.005492918248030520881, 0.006408404622702273783, 0.007323890997374024950 ),
 .UNSPECIFIED. ) ;
#22543=CARTESIAN_POINT ( 'NONE',  ( -3.458734125000000770, 1.432654583217640498, 2.925000001365598123 ) ) ;
#22550=DIRECTION ( 'NONE',  ( -0.000000000000000000, -0.000000000000000000, 1.000000000000000000 ) ) ;
#22553=( NAMED_UNIT ( * ) SI_UNIT ( $, .STERADIAN. ) SOLID_ANGLE_UNIT ( ) );
#22554=CARTESIAN_POINT ( 'NONE',  ( -2.445694354108820523, 2.445694354108820523, 1.612500001365596125 ) ) ;
#22555=CARTESIAN_POINT ( 'NONE',  ( 2.445694354108820079, 2.445694354108820523, 0.3625000013655951259 ) ) ;
#22566=CARTESIAN_POINT ( 'NONE',  ( 4.000000000000000000, 0.000000000000000000, 19.04999999999996874 ) ) ;
#22577=CARTESIAN_POINT ( 'NONE',  ( -1.432654583217640498, 3.458734125000000770, 3.800000001365595459 ) ) ;
#22581=DIRECTION ( 'NONE',  ( 0.000000000000000000, 0.000000000000000000, -1.000000000000000000 ) ) ;
#22585=CARTESIAN_POINT ( 'NONE',  ( 4.000000000000000000, 1.656854249492381248, 3.987500002731185766 ) ) ;
#22599=CARTESIAN_POINT ( 'NONE',  ( 0.000000000000000000, 0.000000000000000000, 19.04999999999996874 ) ) ;
#22603=AXIS2_PLACEMENT_3D ( 'NONE', #21409, #17727, #14266 ) ;
#22632=CARTESIAN_POINT ( 'NONE',  ( 6.499999999999999112, 2.531211054341943711, -0.2595069192555981008 ) ) ;
#22634=CARTESIAN_POINT ( 'NONE',  ( -1.656854249492380804, 4.000000000000000000, 3.112500000000002487 ) ) ;
#22638=EDGE_LOOP ( 'NONE', ( #4755, #10628, #10998, #936 ) ) ;
#22645=ORIENTED_EDGE ( 'NONE', *, *, #12659, .F. ) ;
#22646=ORIENTED_EDGE ( 'NONE', *, *, #21192, .F. ) ;
#22656=CARTESIAN_POINT ( 'NONE',  ( -2.445694354108819635, -2.445694354108820967, 3.112500001365597679 ) ) ;
#22665=CARTESIAN_POINT ( 'NONE',  ( -2.117863837641485618E-16, 3.458734125000000326, 0.4875000013655952369 ) ) ;
#22667=CARTESIAN_POINT ( 'NONE',  ( 3.458734125000000326, 4.235727675282971730E-16, 1.237500001365595903 ) ) ;
#22675=CARTESIAN_POINT ( 'NONE',  ( 1.432654583217640276, 3.458734125000000770, -1.324999998634403209 ) ) ;
#22676=CARTESIAN_POINT ( 'NONE',  ( -5.434916218090831919, -4.367703157927335766, -3.442152416367926460 ) ) ;
#22685=CARTESIAN_POINT ( 'NONE',  ( -3.458734125000000770, 1.432654583217640498, 5.925000001365596347 ) ) ;
#22711=( BOUNDED_CURVE ( )  B_SPLINE_CURVE ( 2, ( #9740, #19279, #2521, #20837, #13686, #8418, #8064, #2757, #22402 ),
 .UNSPECIFIED., .F., .F. ) 
 B_SPLINE_CURVE_WITH_KNOTS ( ( 3, 2, 2, 2, 3 ),
 ( 0.6999999999999999556, 0.7125000000000000222, 0.7249999999999999778, 0.7375000000000000444, 0.7500000000000000000 ),
 .UNSPECIFIED. ) 
 CURVE ( )  GEOMETRIC_REPRESENTATION_ITEM ( )  RATIONAL_B_SPLINE_CURVE ( ( 1.000000000000000000, 0.9238795325112867385, 1.000000000000000000, 0.9238795325112867385, 1.000000000000000000, 0.9238795325112867385, 1.000000000000000000, 0.9238795325112867385, 1.000000000000000000 ) ) 
 REPRESENTATION_ITEM ( '' )  );
#22719=CARTESIAN_POINT ( 'NONE',  ( -4.000000000000000000, 4.898587196589412829E-16, -3.699999999999998401 ) ) ;
#22749=CARTESIAN_POINT ( 'NONE',  ( -4.000000000000000888, 1.656854249492380804, 0.2375000000000018763 ) ) ;
#22754=ORIENTED_EDGE ( 'NONE', *, *, #13319, .F. ) ;
#22759=CARTESIAN_POINT ( 'NONE',  ( 4.000000000000000000, 0.000000000000000000, 19.04999999999996874 ) ) ;
#22773=CARTESIAN_POINT ( 'NONE',  ( -2.445694354108820523, 2.445694354108820523, 3.862500001365594571 ) ) ;
#22783=CARTESIAN_POINT ( 'NONE',  ( -2.445694354108819635, -2.445694354108820523, 0.8625000013655955700 ) ) ;
#22785=CARTESIAN_POINT ( 'NONE',  ( 3.458734125000001214, -1.432654583217639610, -0.8249999986344029868 ) ) ;
#22789=ORIENTED_EDGE ( 'NONE', *, *, #20402, .T. ) ;
#22794=CARTESIAN_POINT ( 'NONE',  ( -2.445694354108820523, 2.445694354108820523, -3.137499998634402765 ) ) ;
#22803=CARTESIAN_POINT ( 'NONE',  ( -3.458734125000000326, 1.432654583217640276, -2.324999998634404097 ) ) ;
#22812=CARTESIAN_POINT ( 'NONE',  ( 7.347880794884118750E-16, -4.000000000000000000, 4.675000002731187543 ) ) ;
#22815=CARTESIAN_POINT ( 'NONE',  ( -2.828427124746189403, -2.828427124746190735, 1.550000002731187765 ) ) ;
#22816=FACE_OUTER_BOUND ( 'NONE', #22995, .T. ) ;
#22817=ORIENTED_EDGE ( 'NONE', *, *, #21184, .F. ) ;
#22847=CARTESIAN_POINT ( 'NONE',  ( 3.250000000000004441, 5.629165124598849879, -3.700000000000000178 ) ) ;
#22853=( BOUNDED_CURVE ( )  B_SPLINE_CURVE ( 2, ( #4960, #12294, #3275, #23272, #3392, #8927, #3151, #6879, #1589 ),
 .UNSPECIFIED., .F., .F. ) 
 B_SPLINE_CURVE_WITH_KNOTS ( ( 3, 2, 2, 2, 3 ),
 ( 0.7500000000000000000, 0.7624999999999999556, 0.7750000000000000222, 0.7874999999999999778, 0.8000000000000000444 ),
 .UNSPECIFIED. ) 
 CURVE ( )  GEOMETRIC_REPRESENTATION_ITEM ( )  RATIONAL_B_SPLINE_CURVE ( ( 1.000000000000000000, 0.9238795325112867385, 1.000000000000000000, 0.9238795325112867385, 1.000000000000000000, 0.9238795325112867385, 1.000000000000000000, 0.9238795325112867385, 1.000000000000000000 ) ) 
 REPRESENTATION_ITEM ( '' )  );
#22867=CARTESIAN_POINT ( 'NONE',  ( -2.325118450655084601, 2.568015399834976176, -3.295601554149325541 ) ) ;
#22877=EDGE_LOOP ( 'NONE', ( #981, #10867, #13951, #11654, #19490, #19601 ) ) ;
#22881=AXIS2_PLACEMENT_3D ( 'NONE', #8554, #19547, #8448 ) ;
#22885=CARTESIAN_POINT ( 'NONE',  ( -1.656854249492380582, 4.000000000000000000, -0.7624999972688126793 ) ) ;
#22895=CARTESIAN_POINT ( 'NONE',  ( 6.353591512924457348E-16, -3.458734125000000770, -0.7624999986344024316 ) ) ;
#22905=CARTESIAN_POINT ( 'NONE',  ( -3.458734124999999882, -1.432654583217642275, 1.800000001365597235 ) ) ;
#22907=CARTESIAN_POINT ( 'NONE',  ( 4.000000000000000000, 4.898587196589412829E-16, -0.1999999999999987899 ) ) ;
#22917=CARTESIAN_POINT ( 'NONE',  ( -3.458734125000000326, -1.432654583217642497, -1.949999998634404097 ) ) ;
#22927=CARTESIAN_POINT ( 'NONE',  ( 6.353591512924457348E-16, -3.458734125000000770, 0.2375000013655967357 ) ) ;
#22933=CARTESIAN_POINT ( 'NONE',  ( -4.000000000000000888, 1.656854249492380582, -1.762499999999997957 ) ) ;
#22937=CARTESIAN_POINT ( 'NONE',  ( -4.000000000000000888, 1.656854249492380804, 2.362500002731187987 ) ) ;
#22942=ADVANCED_FACE ( 'NONE', ( #6386, #2889 ), #13704, .F. ) ;
#22948=PRODUCT_DEFINITION_CONTEXT ( 'detailed design', #11642, 'design' ) ;
#22956=CARTESIAN_POINT ( 'NONE',  ( 3.458734125000000326, 1.432654583217640498, 3.300000001365598568 ) ) ;
#22964=CIRCLE ( 'NONE', #11131, 1.020000000000000018 ) ;
#22978=EDGE_CURVE ( 'NONE', #9522, #21072, #1524, .T. ) ;
#22991=CARTESIAN_POINT ( 'NONE',  ( -4.000000000000000888, 1.656854249492380804, -0.7624999999999970690 ) ) ;
#22995=EDGE_LOOP ( 'NONE', ( #15491, #11091, #22229, #6005, #9301, #1079 ) ) ;
#23012=CARTESIAN_POINT ( 'NONE',  ( 6.500000000000000888, -2.517290933526017405, -0.2565799252183981749 ) ) ;
#23015=CARTESIAN_POINT ( 'NONE',  ( 2.445694354108820079, 2.445694354108820523, 0.6125000013655953479 ) ) ;
#23025=CARTESIAN_POINT ( 'NONE',  ( -6.500000000000000000, 3.752776749732564809, -3.700000000000000178 ) ) ;
#23027=FACE_OUTER_BOUND ( 'NONE', #11487, .T. ) ;
#23028=EDGE_LOOP ( 'NONE', ( #8991, #11960, #13069, #19416, #22646, #13152 ) ) ;
#23042=CARTESIAN_POINT ( 'NONE',  ( -3.458734125000000326, -1.432654583217642497, 1.050000001365596791 ) ) ;
#23048=CARTESIAN_POINT ( 'NONE',  ( -1.656854249492380582, 4.000000000000000000, -1.887499999999998179 ) ) ;
#23051=CARTESIAN_POINT ( 'NONE',  ( -2.828427124746190291, 2.828427124746190291, -0.6999999972688124572 ) ) ;
#23066=CARTESIAN_POINT ( 'NONE',  ( 3.458734125000000326, 1.432654583217640498, 2.300000001365597679 ) ) ;
#23068=FACE_OUTER_BOUND ( 'NONE', #18762, .T. ) ;
#23071=CARTESIAN_POINT ( 'NONE',  ( -3.556935580002248187, 0.06199486344584782122, 2.039999999999997371 ) ) ;
#23072=CARTESIAN_POINT ( 'NONE',  ( -6.500000000000000000, 0.000000000000000000, -3.700000000000000178 ) ) ;
#23091=CARTESIAN_POINT ( 'NONE',  ( -1.656854249492381248, -3.999999999999999112, -1.387499997268811347 ) ) ;
#23104=VERTEX_POINT ( 'NONE', #6853 ) ;
#23119=EDGE_CURVE ( 'NONE', #11906, #14307, #1800, .T. ) ;
#23122=CARTESIAN_POINT ( 'NONE',  ( -2.445694354108820523, 2.445694354108820523, -1.137499998634402765 ) ) ;
#23154=CARTESIAN_POINT ( 'NONE',  ( -2.445694354108819635, -2.445694354108820967, 0.1125000013655966247 ) ) ;
#23155=CARTESIAN_POINT ( 'NONE',  ( -0.6665512827318446076, -3.401344631923079120, 2.039999999999997815 ) ) ;
#23159=ORIENTED_EDGE ( 'NONE', *, *, #14173, .F. ) ;
#23164=CARTESIAN_POINT ( 'NONE',  ( 7.347880794884118750E-16, -4.000000000000000000, -1.324999997268811347 ) ) ;
#23180=CARTESIAN_POINT ( 'NONE',  ( -3.458734124999999882, -1.432654583217642497, 4.800000001365595459 ) ) ;
#23185=CARTESIAN_POINT ( 'NONE',  ( -2.503920655715996979, 2.852548534406722069, 2.039999999999996927 ) ) ;
#23212=CARTESIAN_POINT ( 'NONE',  ( -3.250000000000004441, 5.629165124598849879, 0.000000000000000000 ) ) ;
#23218=CARTESIAN_POINT ( 'NONE',  ( -2.445694354108820523, 2.445694354108820523, -0.3874999986344038194 ) ) ;
#23220=ORIENTED_EDGE ( 'NONE', *, *, #12946, .T. ) ;
#23223=AXIS2_PLACEMENT_3D ( 'NONE', #18554, #6227, #9834 ) ;
#23239=CARTESIAN_POINT ( 'NONE',  ( -3.458734125000000326, -1.432654583217642497, -1.949999998634404319 ) ) ;
#23244=VECTOR ( 'NONE', #637, 1000.000000000000000 ) ;
#23272=CARTESIAN_POINT ( 'NONE',  ( 1.656854249492383024, -3.999999999999999112, -2.262499997268812013 ) ) ;
#23276=CARTESIAN_POINT ( 'NONE',  ( -2.445694354108819635, -2.445694354108820967, 1.112500001365595681 ) ) ;
#23286=CARTESIAN_POINT ( 'NONE',  ( 4.000000000000000000, 1.656854249492381248, 0.9875000027311869877 ) ) ;
#23305=CARTESIAN_POINT ( 'NONE',  ( 0.000000000000000000, 0.000000000000000000, 0.000000000000000000 ) ) ;
#23309=CARTESIAN_POINT ( 'NONE',  ( -3.458734125000000326, 1.432654583217640276, 5.675000001365596347 ) ) ;
#23315=CARTESIAN_POINT ( 'NONE',  ( -0.9451720798219458430, 3.813322425661201276, 2.039999999999999147 ) ) ;
#23337=CARTESIAN_POINT ( 'NONE',  ( 0.000000000000000000, 0.000000000000000000, -3.700000000000000178 ) ) ;
#23346=CARTESIAN_POINT ( 'NONE',  ( 1.656854249492383024, -3.999999999999999112, -1.387499999999997513 ) ) ;
#23352=CARTESIAN_POINT ( 'NONE',  ( -2.445694354108820523, 2.445694354108820523, -1.387499998634402987 ) ) ;
#23358=CARTESIAN_POINT ( 'NONE',  ( -6.500000000000000000, 3.752776749732564809, -0.5805565836007661185 ) ) ;
#23370=CARTESIAN_POINT ( 'NONE',  ( 6.353591512924457348E-16, -3.458734125000000770, 1.237500001365595903 ) ) ;
#23382=CARTESIAN_POINT ( 'NONE',  ( -2.117863837641485618E-16, 3.458734125000000326, -2.512499998634404097 ) ) ;
#23398=CARTESIAN_POINT ( 'NONE',  ( -2.445694354108820523, 2.445694354108820523, -3.137499998634402765 ) ) ;
#23399=FACE_OUTER_BOUND ( 'NONE', #1614, .T. ) ;
#23407=CARTESIAN_POINT ( 'NONE',  ( -2.449293598294706907E-16, 4.000000000000000000, 2.175000002731188431 ) ) ;
#23414=DIRECTION ( 'NONE',  ( 0.000000000000000000, 0.000000000000000000, 1.000000000000000000 ) ) ;
#23428=CARTESIAN_POINT ( 'NONE',  ( 1.432654583217642275, -3.458734124999999437, 5.050000001365596347 ) ) ;
#23430=B_SPLINE_CURVE_WITH_KNOTS ( 'NONE', 3,
 ( #8629, #10447, #15932, #6821, #16171, #14144 ),
 .UNSPECIFIED., .F., .F.,
 ( 4, 2, 4 ),
 ( 0.006695446894088490607, 0.008593684019695168111, 0.01049192114530184475 ),
 .UNSPECIFIED. ) ;
#23435=DIRECTION ( 'NONE',  ( -1.000000000000000000, 1.776356839400250465E-15, 0.000000000000000000 ) ) ;
#23438=EDGE_CURVE ( 'NONE', #6397, #10129, #19140, .T. ) ;
#23461=CIRCLE ( 'NONE', #2804, 4.714285714285714413 ) ;
#23468=CARTESIAN_POINT ( 'NONE',  ( -2.445694354108819635, -2.445694354108820523, -1.137499998634402765 ) ) ;
#23483=CARTESIAN_POINT ( 'NONE',  ( 1.656854249492383024, -3.999999999999999112, 5.612500000000003375 ) ) ;
#23493=CARTESIAN_POINT ( 'NONE',  ( -2.445694354108820523, 2.445694354108820523, -2.387499998634403653 ) ) ;
#23494=ORIENTED_EDGE ( 'NONE', *, *, #10533, .T. ) ;
#23522=CARTESIAN_POINT ( 'NONE',  ( 7.347880794884118750E-16, -4.000000000000000000, 0.6750000027311870987 ) ) ;
#23545=CARTESIAN_POINT ( 'NONE',  ( -3.458734125000000326, 1.432654583217640276, 1.675000001365597235 ) ) ;
#23555=CARTESIAN_POINT ( 'NONE',  ( -6.499999999999999112, 7.960204194457794491E-16, 9.480888224575631185 ) ) ;
#23560=EDGE_CURVE ( 'NONE', #7525, #11761, #2987, .T. ) ;
#23561=ORIENTED_EDGE ( 'NONE', *, *, #22978, .F. ) ;
#23565=ORIENTED_EDGE ( 'NONE', *, *, #1907, .F. ) ;
#23580=CARTESIAN_POINT ( 'NONE',  ( -0.5316568767328819778, -7.198601258566901251, -0.4033376246892538264 ) ) ;
#23588=CARTESIAN_POINT ( 'NONE',  ( -2.445694354108819635, -2.445694354108820523, -2.137499998634403653 ) ) ;
#23607=CARTESIAN_POINT ( 'NONE',  ( -4.000000000000000888, 1.656854249492380804, 5.237500000000000711 ) ) ;
#23620=CARTESIAN_POINT ( 'NONE',  ( 2.445694354108820079, 2.445694354108820523, -2.637499998634404097 ) ) ;
#23645=CARTESIAN_POINT ( 'NONE',  ( 1.432654583217642275, -3.458734124999999437, 5.050000001365596347 ) ) ;
#23658=CARTESIAN_POINT ( 'NONE',  ( -1.432654583217640498, 3.458734125000000770, 1.800000001365597235 ) ) ;
#23664=CARTESIAN_POINT ( 'NONE',  ( -3.458734124999999882, -1.432654583217642497, -0.1999999986344043745 ) ) ;
#23682=DIRECTION ( 'NONE',  ( -0.000000000000000000, -0.000000000000000000, 1.000000000000000000 ) ) ;
#23690=DIRECTION ( 'NONE',  ( -0.000000000000000000, -0.000000000000000000, 1.000000000000000000 ) ) ;
ENDSEC;
END-ISO-10303-21;
